ISO-10303-21;
HEADER;
FILE_DESCRIPTION (('STEP AP203'),
    '1' );
FILE_NAME ('Part8_handle2Sleeve.step',
    '2026-10-06T15:07:10',
    ( '' ),
    ( '' ),
    'SwSTEP 2.0',
    'SolidWorks 2024',
    '' );
FILE_SCHEMA (( 'AUTOMOTIVE_DESIGN' ));
ENDSEC;

DATA;
#78=DIRECTION ( 'NONE',  ( -0.000000000000000000, -0.000000000000000000, -1.000000000000000000 ) ) ;
#121=CARTESIAN_POINT ( 'NONE',  ( 108.6457025336241031, 16.11621187055573046, -2.334455007174250696 ) ) ;
#160=CARTESIAN_POINT ( 'NONE',  ( 56.97280603064898941, -277.2763395528616002, 4.999054092451761022 ) ) ;
#162=AXIS2_PLACEMENT_3D ( 'NONE', #23286, #22786, #32990 ) ;
#218=ORIENTED_EDGE ( 'NONE', *, *, #6090, .F. ) ;
#284=CARTESIAN_POINT ( 'NONE',  ( 108.7297614063222113, 16.58428484178596207, 3.222654696952877096 ) ) ;
#305=ORIENTED_EDGE ( 'NONE', *, *, #17119, .F. ) ;
#307=CARTESIAN_POINT ( 'NONE',  ( 25.86240141410256044, 23.76612641949138549, -0.4463807625373443777 ) ) ;
#335=DIRECTION ( 'NONE',  ( -0.000000000000000000, -0.000000000000000000, -1.000000000000000000 ) ) ;
#343=ORIENTED_EDGE ( 'NONE', *, *, #19267, .T. ) ;
#389=VERTEX_POINT ( 'NONE', #29371 ) ;
#401=CARTESIAN_POINT ( 'NONE',  ( 109.3993806922052840, 20.31298924473512457, -2.334455007174283558 ) ) ;
#404=CARTESIAN_POINT ( 'NONE',  ( 110.6444052656891301, 21.58830278953161752, -0.4463807625373402699 ) ) ;
#430=DIRECTION ( 'NONE',  ( -1.000000000000000000, 0.000000000000000000, 0.000000000000000000 ) ) ;
#469=VERTEX_POINT ( 'NONE', #6960 ) ;
#479=FACE_OUTER_BOUND ( 'NONE', #18450, .T. ) ;
#486=EDGE_LOOP ( 'NONE', ( #3638, #26614, #7912, #9286 ) ) ;
#526=EDGE_CURVE ( 'NONE', #4621, #9325, #17910, .T. ) ;
#573=CARTESIAN_POINT ( 'NONE',  ( 109.4759884372992076, 20.73957139739071209, 1.099690583642431996 ) ) ;
#609=DIRECTION ( 'NONE',  ( -0.000000000000000000, -0.000000000000000000, -1.000000000000000000 ) ) ;
#639=AXIS2_PLACEMENT_3D ( 'NONE', #9264, #19485, #29678 ) ;
#641=AXIS2_PLACEMENT_3D ( 'NONE', #19095, #4668, #2156 ) ;
#658=CIRCLE ( 'NONE', #13443, 0.8000000000000182521 ) ;
#688=ORIENTED_EDGE ( 'NONE', *, *, #22874, .T. ) ;
#692=EDGE_CURVE ( 'NONE', #389, #11133, #17844, .T. ) ;
#709=FACE_OUTER_BOUND ( 'NONE', #8742, .T. ) ;
#802=DIRECTION ( 'NONE',  ( 0.9842544651762055175, -0.1767573132311700268, 0.000000000000000000 ) ) ;
#895=CYLINDRICAL_SURFACE ( 'NONE', #10132, 297.4345239564032681 ) ;
#917=EDGE_CURVE ( 'NONE', #21913, #11133, #25114, .T. ) ;
#1004=ORIENTED_EDGE ( 'NONE', *, *, #10378, .T. ) ;
#1034=EDGE_CURVE ( 'NONE', #3368, #31265, #2709, .T. ) ;
#1039=CARTESIAN_POINT ( 'NONE',  ( 25.75960661490314507, 24.76082900280850652, -0.4463807625373402699 ) ) ;
#1061=AXIS2_PLACEMENT_3D ( 'NONE', #5420, #20648, #10437 ) ;
#1129=DIRECTION ( 'NONE',  ( 0.9842544651762055175, -0.1767573132311700268, 0.000000000000000000 ) ) ;
#1157=DIRECTION ( 'NONE',  ( -1.000000000000000000, 0.000000000000000000, 0.000000000000000000 ) ) ;
#1270=ADVANCED_FACE ( 'NONE', ( #12481 ), #5885, .F. ) ;
#1290=CARTESIAN_POINT ( 'NONE',  ( 109.7266016284591927, 16.47760998941501143, 5.471072653610988823 ) ) ;
#1309=EDGE_CURVE ( 'NONE', #8686, #389, #31550, .T. ) ;
#1319=DIRECTION ( 'NONE',  ( -1.000000000000000000, 0.000000000000000000, 0.000000000000000000 ) ) ;
#1323=ORIENTED_EDGE ( 'NONE', *, *, #22495, .F. ) ;
#1327=CARTESIAN_POINT ( 'NONE',  ( 108.5619817448483531, 15.65002148400675530, 0.7764623223310612721 ) ) ;
#1470=CARTESIAN_POINT ( 'NONE',  ( 56.97280603064904625, -277.2763395528616002, 554.0683451991844777 ) ) ;
#1561=EDGE_LOOP ( 'NONE', ( #17178, #14253, #1004, #18496 ) ) ;
#1787=VECTOR ( 'NONE', #25428, 1000.000000000000000 ) ;
#1793=CARTESIAN_POINT ( 'NONE',  ( 56.97280603064898941, -277.2763395528616002, -5.471072653611070535 ) ) ;
#1885=FACE_OUTER_BOUND ( 'NONE', #29245, .T. ) ;
#1960=DIRECTION ( 'NONE',  ( -1.000000000000000000, 0.000000000000000000, 0.000000000000000000 ) ) ;
#1964=CARTESIAN_POINT ( 'NONE',  ( 25.98690466878739613, 22.56136012750964426, -0.4463807625373771293 ) ) ;
#1967=DIRECTION ( 'NONE',  ( -0.1027947991993876792, 0.9947025833170222153, 0.000000000000000000 ) ) ;
#1998=ADVANCED_FACE ( 'NONE', ( #29753 ), #10831, .T. ) ;
#2033=DIRECTION ( 'NONE',  ( 0.9947025833170223263, 0.1027947991993880261, 0.000000000000000000 ) ) ;
#2079=CARTESIAN_POINT ( 'NONE',  ( 108.7297614063222113, 16.58428484178599405, -3.222654696952903741 ) ) ;
#2104=DIRECTION ( 'NONE',  ( 1.000000000000000000, 0.000000000000000000, 0.000000000000000000 ) ) ;
#2122=CARTESIAN_POINT ( 'NONE',  ( 110.6444052656891159, 21.58830278953162107, -0.4463807625373413246 ) ) ;
#2146=ORIENTED_EDGE ( 'NONE', *, *, #25842, .T. ) ;
#2156=DIRECTION ( 'NONE',  ( -1.000000000000000000, 0.000000000000000000, 0.000000000000000000 ) ) ;
#2177=AXIS2_PLACEMENT_3D ( 'NONE', #4127, #19833, #24670 ) ;
#2186=DIRECTION ( 'NONE',  ( -0.04852105321274767513, 0.4695180821586621978, -0.8815886103626665582 ) ) ;
#2231=CIRCLE ( 'NONE', #23030, 297.9081695149526468 ) ;
#2310=CARTESIAN_POINT ( 'NONE',  ( 109.4744264295851082, 15.07339897850246579, -2.806473568333506474 ) ) ;
#2329=CARTESIAN_POINT ( 'NONE',  ( 56.97280603064898941, -277.2763395528616002, -0.4463807625373593657 ) ) ;
#2360=DIRECTION ( 'NONE',  ( 0.9842544651762055175, -0.1767573132311700268, 0.000000000000000000 ) ) ;
#2367=ADVANCED_FACE ( 'NONE', ( #24683 ), #29210, .F. ) ;
#2411=DIRECTION ( 'NONE',  ( -1.000000000000000000, 0.000000000000000000, 0.000000000000000000 ) ) ;
#2414=ADVANCED_BREP_SHAPE_REPRESENTATION ( '', ( #9961, #2865 ), #30610 ) ;
#2504=CARTESIAN_POINT ( 'NONE',  ( 109.1472041058640912, 18.90877050785832836, -4.999054092451833853 ) ) ;
#2545=EDGE_CURVE ( 'NONE', #22465, #24269, #28540, .T. ) ;
#2574=ORIENTED_EDGE ( 'NONE', *, *, #27807, .T. ) ;
#2614=VERTEX_POINT ( 'NONE', #3131 ) ;
#2615=VERTEX_POINT ( 'NONE', #23494 ) ;
#2709=CIRCLE ( 'NONE', #18697, 302.1720608278466216 ) ;
#2740=AXIS2_PLACEMENT_3D ( 'NONE', #6951, #27363, #20177 ) ;
#2795=VERTEX_POINT ( 'NONE', #6916 ) ;
#2796=AXIS2_PLACEMENT_3D ( 'NONE', #21405, #24245, #24058 ) ;
#2799=CIRCLE ( 'NONE', #25741, 303.0536494382092769 ) ;
#2806=VERTEX_POINT ( 'NONE', #14928 ) ;
#2847=B_SPLINE_CURVE_WITH_KNOTS ( 'NONE', 3,
 ( #8104, #12957, #284, #10455 ),
 .UNSPECIFIED., .F., .F.,
 ( 4, 4 ),
 ( 0.000000000000000000, 0.003022500951957888399 ),
 .UNSPECIFIED. ) ;
#2864=CARTESIAN_POINT ( 'NONE',  ( 108.6457025336241031, 16.11621187055573046, 2.334455007174216057 ) ) ;
#2865=AXIS2_PLACEMENT_3D ( 'NONE', #14796, #7619, #2104 ) ;
#2895=ORIENTED_EDGE ( 'NONE', *, *, #7336, .T. ) ;
#2951=CYLINDRICAL_SURFACE ( 'NONE', #22433, 302.6457063863960002 ) ;
#2982=ORIENTED_EDGE ( 'NONE', *, *, #8207, .F. ) ;
#3003=CARTESIAN_POINT ( 'NONE',  ( 110.2875796713736634, 19.60135708372762409, -5.471072653611070535 ) ) ;
#3014=DIRECTION ( 'NONE',  ( 1.000000000000000000, 7.164576672270377148E-15, 0.000000000000000000 ) ) ;
#3027=CARTESIAN_POINT ( 'NONE',  ( 108.6181628067467386, 15.96285980464529786, -2.043459231428901735 ) ) ;
#3047=EDGE_CURVE ( 'NONE', #4554, #11141, #15487, .T. ) ;
#3061=ORIENTED_EDGE ( 'NONE', *, *, #5068, .F. ) ;
#3116=CARTESIAN_POINT ( 'NONE',  ( 26.20274081918675435, 20.47280333234591154, 4.999054092451758358 ) ) ;
#3131=CARTESIAN_POINT ( 'NONE',  ( 110.2875796713736918, 19.60135708372767382, 5.471072653610979941 ) ) ;
#3134=CARTESIAN_POINT ( 'NONE',  ( 56.97280603064898941, -277.2763395528616002, 5.471072653610988823 ) ) ;
#3177=CARTESIAN_POINT ( 'NONE',  ( 26.39808386558502917, 18.58254979424145503, -0.4463807625373593657 ) ) ;
#3183=ORIENTED_EDGE ( 'NONE', *, *, #17906, .F. ) ;
#3193=ORIENTED_EDGE ( 'NONE', *, *, #2545, .F. ) ;
#3204=DIRECTION ( 'NONE',  ( 0.1027947991993881510, -0.9947025833170222153, -3.252606517456439149E-15 ) ) ;
#3213=AXIS2_PLACEMENT_3D ( 'NONE', #20669, #7943, #430 ) ;
#3235=CARTESIAN_POINT ( 'NONE',  ( 56.97280603064898941, -277.2763395528616002, -5.471072653611049219 ) ) ;
#3249=AXIS2_PLACEMENT_3D ( 'NONE', #3134, #609, #15662 ) ;
#3330=CARTESIAN_POINT ( 'NONE',  ( 109.3993806922052698, 20.31298924473501444, 2.334455007174201402 ) ) ;
#3368=VERTEX_POINT ( 'NONE', #32408 ) ;
#3458=CARTESIAN_POINT ( 'NONE',  ( 26.39808386558502562, 18.58254979424150832, 0.4463807625373201193 ) ) ;
#3472=LINE ( 'NONE', #23678, #8581 ) ;
#3476=EDGE_CURVE ( 'NONE', #4283, #18871, #4830, .T. ) ;
#3478=DIRECTION ( 'NONE',  ( -0.08343273266574553759, -0.4645863764670123963, 0.8815886103626666692 ) ) ;
#3556=DIRECTION ( 'NONE',  ( 0.1027947991993877208, -0.9947025833170222153, 0.000000000000000000 ) ) ;
#3563=ORIENTED_EDGE ( 'NONE', *, *, #22450, .T. ) ;
#3608=CARTESIAN_POINT ( 'NONE',  ( 109.3993806922052840, 20.31298924473512457, -2.334455007174283558 ) ) ;
#3638=ORIENTED_EDGE ( 'NONE', *, *, #32426, .T. ) ;
#3641=EDGE_CURVE ( 'NONE', #22465, #17163, #32066, .T. ) ;
#3677=ORIENTED_EDGE ( 'NONE', *, *, #31861, .T. ) ;
#3689=ORIENTED_EDGE ( 'NONE', *, *, #31553, .F. ) ;
#3768=B_SPLINE_CURVE_WITH_KNOTS ( 'NONE', 3,
 ( #3330, #11151, #7995, #18190 ),
 .UNSPECIFIED., .F., .F.,
 ( 4, 4 ),
 ( 0.000000000000000000, 0.003022500881216731543 ),
 .UNSPECIFIED. ) ;
#3807=LINE ( 'NONE', #14158, #11914 ) ;
#3879=CONICAL_SURFACE ( 'NONE', #15615, 302.1720608278466216, 0.4915790642873723582 ) ;
#3918=ORIENTED_EDGE ( 'NONE', *, *, #18926, .T. ) ;
#3945=DIRECTION ( 'NONE',  ( 0.000000000000000000, 0.000000000000000000, 1.000000000000000000 ) ) ;
#3969=DIRECTION ( 'NONE',  ( -0.1027947991993878318, 0.9947025833170222153, 0.000000000000000000 ) ) ;
#3993=EDGE_LOOP ( 'NONE', ( #29139, #16692, #29408, #32639 ) ) ;
#4003=ORIENTED_EDGE ( 'NONE', *, *, #11041, .T. ) ;
#4127=CARTESIAN_POINT ( 'NONE',  ( 56.97280603064898941, -277.2763395528616002, -4.621439243524461560 ) ) ;
#4160=ORIENTED_EDGE ( 'NONE', *, *, #18307, .T. ) ;
#4176=DIRECTION ( 'NONE',  ( 0.9842544651762055175, -0.1767573132311700268, 0.000000000000000000 ) ) ;
#4256=AXIS2_PLACEMENT_3D ( 'NONE', #16448, #9084, #11117 ) ;
#4283=VERTEX_POINT ( 'NONE', #20417 ) ;
#4322=CARTESIAN_POINT ( 'NONE',  ( 109.4757865442224443, 20.73844717707612872, -1.106576248373506655 ) ) ;
#4371=CARTESIAN_POINT ( 'NONE',  ( 56.97280603064898941, -277.2763395528616002, -5.471072653611063430 ) ) ;
#4401=AXIS2_PLACEMENT_3D ( 'NONE', #12060, #17243, #27445 ) ;
#4414=CLOSED_SHELL ( 'NONE', ( #8963, #5866, #15214, #16706, #1998, #8735, #11094, #9310, #32964, #22541, #13934, #8865, #2367, #27788, #33066, #23886, #16101, #17549, #5293, #22009, #32301, #1270, #19495, #23457, #23706, #20413, #10270 ) ) ;
#4425=EDGE_CURVE ( 'NONE', #3368, #15820, #8076, .T. ) ;
#4435=AXIS2_PLACEMENT_3D ( 'NONE', #8010, #5347, #28092 ) ;
#4446=CIRCLE ( 'NONE', #639, 297.9081695149526468 ) ;
#4477=CARTESIAN_POINT ( 'NONE',  ( 56.97280603064898941, -277.2763395528616002, -4.999054092451827636 ) ) ;
#4500=EDGE_LOOP ( 'NONE', ( #30114, #13348, #31409, #21095 ) ) ;
#4546=ORIENTED_EDGE ( 'NONE', *, *, #17931, .T. ) ;
#4554=VERTEX_POINT ( 'NONE', #17994 ) ;
#4604=CARTESIAN_POINT ( 'NONE',  ( 109.3697760341437828, 14.49066428361113346, 0.4463807625373157340 ) ) ;
#4621=VERTEX_POINT ( 'NONE', #3458 ) ;
#4652=CARTESIAN_POINT ( 'NONE',  ( 56.97280603064904625, -277.2763395528616002, -554.0683451992334767 ) ) ;
#4668=DIRECTION ( 'NONE',  ( -0.000000000000000000, -0.000000000000000000, -1.000000000000000000 ) ) ;
#4682=ORIENTED_EDGE ( 'NONE', *, *, #15933, .T. ) ;
#4704=ORIENTED_EDGE ( 'NONE', *, *, #18789, .T. ) ;
#4705=EDGE_CURVE ( 'NONE', #11560, #19335, #23909, .T. ) ;
#4733=CARTESIAN_POINT ( 'NONE',  ( 25.75960661490314507, 24.76082900280850652, 0.4463807625372899768 ) ) ;
#4741=DIRECTION ( 'NONE',  ( -1.000000000000000000, 0.000000000000000000, 0.000000000000000000 ) ) ;
#4748=ORIENTED_EDGE ( 'NONE', *, *, #1309, .F. ) ;
#4809=DIRECTION ( 'NONE',  ( 0.04852105321274372690, -0.4695180821586373288, -0.8815886103626799919 ) ) ;
#4825=VERTEX_POINT ( 'NONE', #404 ) ;
#4830=CIRCLE ( 'NONE', #29378, 4.000000000000000000 ) ;
#4846=AXIS2_PLACEMENT_3D ( 'NONE', #25052, #2360, #5181 ) ;
#4855=DIRECTION ( 'NONE',  ( -0.1027947991993878041, 0.9947025833170222153, 0.000000000000000000 ) ) ;
#4887=AXIS2_PLACEMENT_3D ( 'NONE', #29401, #24230, #14182 ) ;
#4908=AXIS2_PLACEMENT_3D ( 'NONE', #9371, #19581, #6856 ) ;
#4927=CIRCLE ( 'NONE', #17723, 4.999999999999998224 ) ;
#5010=VECTOR ( 'NONE', #28207, 1000.000000000000114 ) ;
#5068=EDGE_CURVE ( 'NONE', #469, #30909, #15596, .T. ) ;
#5077=EDGE_CURVE ( 'NONE', #15820, #28329, #27334, .T. ) ;
#5121=CARTESIAN_POINT ( 'NONE',  ( 56.97280603064898941, -277.2763395528616002, 0.4463807625373348298 ) ) ;
#5132=CARTESIAN_POINT ( 'NONE',  ( 26.27358061090008690, 19.78731608622338101, 0.4463807625373084065 ) ) ;
#5137=B_SPLINE_CURVE_WITH_KNOTS ( 'NONE', 3,
 ( #23441, #25814, #23297, #401 ),
 .UNSPECIFIED., .F., .F.,
 ( 4, 4 ),
 ( 0.000000000000000000, 0.003022500881216829988 ),
 .UNSPECIFIED. ) ;
#5139=DIRECTION ( 'NONE',  ( -0.000000000000000000, -0.000000000000000000, -1.000000000000000000 ) ) ;
#5167=CARTESIAN_POINT ( 'NONE',  ( 108.9715489600704501, 17.93065334586892234, -5.381233285085805562 ) ) ;
#5180=ORIENTED_EDGE ( 'NONE', *, *, #15298, .T. ) ;
#5181=DIRECTION ( 'NONE',  ( -0.1767573132311711093, -0.9842544651762052954, 0.000000000000000000 ) ) ;
#5208=DIRECTION ( 'NONE',  ( 0.000000000000000000, 0.000000000000000000, 1.000000000000000000 ) ) ;
#5293=ADVANCED_FACE ( 'NONE', ( #20867 ), #14504, .F. ) ;
#5326=EDGE_CURVE ( 'NONE', #15255, #7000, #23071, .T. ) ;
#5328=EDGE_CURVE ( 'NONE', #30909, #16263, #28418, .T. ) ;
#5347=DIRECTION ( 'NONE',  ( 0.9842544651762055175, -0.1767573132311700268, 0.000000000000000000 ) ) ;
#5352=DIRECTION ( 'NONE',  ( -0.000000000000000000, -0.000000000000000000, -1.000000000000000000 ) ) ;
#5395=CARTESIAN_POINT ( 'NONE',  ( 25.96712173632212384, 22.75279134953756355, 5.471072653610979941 ) ) ;
#5405=B_SPLINE_CURVE_WITH_KNOTS ( 'NONE', 3,
 ( #30930, #12842, #13182, #31098, #3027, #18390 ),
 .UNSPECIFIED., .F., .F.,
 ( 4, 2, 4 ),
 ( 0.000000000000000000, 0.0009761895969867609435, 0.001952379193973521887 ),
 .UNSPECIFIED. ) ;
#5420=CARTESIAN_POINT ( 'NONE',  ( 56.97280603064898941, -277.2763395528616002, -2.806473568333505586 ) ) ;
#5465=DIRECTION ( 'NONE',  ( 0.04852105321274541305, -0.4695180821586529829, -0.8815886103626715542 ) ) ;
#5504=CARTESIAN_POINT ( 'NONE',  ( 56.97280603064898941, -277.2763395528616002, -2.334455007174283558 ) ) ;
#5508=AXIS2_PLACEMENT_3D ( 'NONE', #5725, #18584, #3556 ) ;
#5597=CARTESIAN_POINT ( 'NONE',  ( 26.13024263984378592, 21.17433810686643980, -4.621439243524461560 ) ) ;
#5599=ORIENTED_EDGE ( 'NONE', *, *, #3047, .T. ) ;
#5694=DIRECTION ( 'NONE',  ( -0.000000000000000000, -0.000000000000000000, -1.000000000000000000 ) ) ;
#5710=CARTESIAN_POINT ( 'NONE',  ( 26.13024263984371842, 21.17433810686647533, 4.621439243524390506 ) ) ;
#5725=CARTESIAN_POINT ( 'NONE',  ( 26.27358061090008690, 19.78731608622338101, -0.4463807625373608645 ) ) ;
#5737=DIRECTION ( 'NONE',  ( -0.000000000000000000, -0.000000000000000000, -1.000000000000000000 ) ) ;
#5781=ORIENTED_EDGE ( 'NONE', *, *, #10179, .T. ) ;
#5866=ADVANCED_FACE ( 'NONE', ( #21314 ), #11192, .T. ) ;
#5885=CONICAL_SURFACE ( 'NONE', #24559, 300.7453860596896789, 0.4915790642873871796 ) ;
#5922=ORIENTED_EDGE ( 'NONE', *, *, #25842, .F. ) ;
#6045=AXIS2_PLACEMENT_3D ( 'NONE', #30581, #7664, #9651 ) ;
#6090=EDGE_CURVE ( 'NONE', #28814, #27014, #7264, .T. ) ;
#6133=EDGE_CURVE ( 'NONE', #18871, #15255, #25986, .T. ) ;
#6241=CARTESIAN_POINT ( 'NONE',  ( 56.97280603064904625, -277.2763395528616002, -566.7009208965738480 ) ) ;
#6330=CARTESIAN_POINT ( 'NONE',  ( 109.7266016284592069, 16.47760998941509669, -5.471072653611049219 ) ) ;
#6377=DIRECTION ( 'NONE',  ( 0.1027947991993876792, -0.9947025833170222153, 0.000000000000000000 ) ) ;
#6469=DIRECTION ( 'NONE',  ( -0.000000000000000000, -0.000000000000000000, -1.000000000000000000 ) ) ;
#6494=ORIENTED_EDGE ( 'NONE', *, *, #31084, .T. ) ;
#6515=CARTESIAN_POINT ( 'NONE',  ( 26.05774446050081750, 21.87587288138697872, 4.999054092451761022 ) ) ;
#6522=CARTESIAN_POINT ( 'NONE',  ( 110.2875796713736776, 19.60135708372761343, -5.471072653611063430 ) ) ;
#6625=CARTESIAN_POINT ( 'NONE',  ( 56.97280603064898941, -277.2763395528616002, 0.4463807625372899768 ) ) ;
#6633=DIRECTION ( 'NONE',  ( 0.1027947991993878873, -0.9947025833170223263, 0.000000000000000000 ) ) ;
#6645=DIRECTION ( 'NONE',  ( -0.04852105321274703675, 0.4695180821586693587, -0.8815886103626627834 ) ) ;
#6656=SHAPE_REPRESENTATION ( 'Part8_handle2Sleeve', ( #2865 ), #30610 ) ;
#6665=CARTESIAN_POINT ( 'NONE',  ( 108.9099939950573912, 17.58789101224671469, 5.127064438068912544 ) ) ;
#6667=CARTESIAN_POINT ( 'NONE',  ( 109.4476176138146002, 20.58159145763585940, -1.739510325230362309 ) ) ;
#6856=DIRECTION ( 'NONE',  ( -1.000000000000000000, 0.000000000000000000, 0.000000000000000000 ) ) ;
#6916=CARTESIAN_POINT ( 'NONE',  ( 26.05774446050084237, 21.87587288138687214, -4.999054092451833853 ) ) ;
#6951=CARTESIAN_POINT ( 'NONE',  ( 56.97280603064898941, -277.2763395528616002, -2.806473568333505142 ) ) ;
#6960=CARTESIAN_POINT ( 'NONE',  ( 26.29336354336542314, 19.59588486419538711, -5.471072653611049219 ) ) ;
#6995=CARTESIAN_POINT ( 'NONE',  ( 56.97280603064898941, -277.2763395528616002, 2.806473568333438084 ) ) ;
#7000=VERTEX_POINT ( 'NONE', #11619 ) ;
#7087=EDGE_CURVE ( 'NONE', #18253, #11141, #29418, .T. ) ;
#7150=CARTESIAN_POINT ( 'NONE',  ( 108.5619817448483531, 15.65002148400673754, 0.4463807625373211185 ) ) ;
#7169=CARTESIAN_POINT ( 'NONE',  ( 109.0480074564792261, 18.35640442295476404, 5.421406144741463429 ) ) ;
#7264=LINE ( 'NONE', #32368, #28807 ) ;
#7268=CARTESIAN_POINT ( 'NONE',  ( 56.97280603064898941, -277.2763395528616002, -2.334455007174276009 ) ) ;
#7291=ORIENTED_EDGE ( 'NONE', *, *, #12199, .T. ) ;
#7317=CARTESIAN_POINT ( 'NONE',  ( 109.1472041058641196, 18.90877050785844204, 4.999054092451761022 ) ) ;
#7331=DIRECTION ( 'NONE',  ( -0.000000000000000000, -0.000000000000000000, -1.000000000000000000 ) ) ;
#7336=EDGE_CURVE ( 'NONE', #18871, #21569, #16057, .T. ) ;
#7355=PRODUCT_DEFINITION_SHAPE ( 'NONE', 'NONE',  #31711 ) ;
#7389=DIRECTION ( 'NONE',  ( 0.9947025833170223263, 0.1027947991993880261, 0.000000000000000000 ) ) ;
#7394=EDGE_LOOP ( 'NONE', ( #19378, #9466, #28339, #27795 ) ) ;
#7405=ORIENTED_EDGE ( 'NONE', *, *, #15000, .F. ) ;
#7564=CIRCLE ( 'NONE', #32691, 297.4345239564032681 ) ;
#7613=AXIS2_PLACEMENT_3D ( 'NONE', #20275, #30830, #2411 ) ;
#7619=DIRECTION ( 'NONE',  ( 0.000000000000000000, 0.000000000000000000, 1.000000000000000000 ) ) ;
#7628=ORIENTED_EDGE ( 'NONE', *, *, #14685, .F. ) ;
#7640=LINE ( 'NONE', #7150, #29526 ) ;
#7664=DIRECTION ( 'NONE',  ( -0.000000000000000000, -0.000000000000000000, -1.000000000000000000 ) ) ;
#7706=PRODUCT_DEFINITION_FORMATION_WITH_SPECIFIED_SOURCE ( 'ANY', '', #22028, .NOT_KNOWN. ) ;
#7765=ORIENTED_EDGE ( 'NONE', *, *, #22450, .F. ) ;
#7780=CARTESIAN_POINT ( 'NONE',  ( 56.97280603064898941, -277.2763395528616002, 2.334455007174201402 ) ) ;
#7794=( LENGTH_UNIT ( ) NAMED_UNIT ( * ) SI_UNIT ( .MILLI., .METRE. ) );
#7839=DIRECTION ( 'NONE',  ( -1.000000000000000000, 0.000000000000000000, 0.000000000000000000 ) ) ;
#7912=ORIENTED_EDGE ( 'NONE', *, *, #3641, .F. ) ;
#7919=DIRECTION ( 'NONE',  ( 0.04852105321274706451, -0.4695180821586696363, 0.8815886103626625614 ) ) ;
#7926=FACE_OUTER_BOUND ( 'NONE', #7394, .T. ) ;
#7943=DIRECTION ( 'NONE',  ( -0.000000000000000000, -0.000000000000000000, -1.000000000000000000 ) ) ;
#7975=DIRECTION ( 'NONE',  ( -0.1767573132311699990, -0.9842544651762054064, 0.000000000000000000 ) ) ;
#7995=CARTESIAN_POINT ( 'NONE',  ( 109.2312629696830015, 19.37684342964560003, 4.110854402524375395 ) ) ;
#8010=CARTESIAN_POINT ( 'NONE',  ( 110.2535626002996310, 19.41193660949216238, 0.4463807625373348298 ) ) ;
#8076=CIRCLE ( 'NONE', #4887, 4.000000000000000000 ) ;
#8104=CARTESIAN_POINT ( 'NONE',  ( 108.8978791464556508, 17.52043075494136204, 4.999054092451758358 ) ) ;
#8169=AXIS2_PLACEMENT_3D ( 'NONE', #21418, #26285, #13561 ) ;
#8170=ORIENTED_EDGE ( 'NONE', *, *, #23425, .F. ) ;
#8207=EDGE_CURVE ( 'NONE', #28814, #17955, #22557, .T. ) ;
#8295=ORIENTED_EDGE ( 'NONE', *, *, #23425, .T. ) ;
#8314=ORIENTED_EDGE ( 'NONE', *, *, #27856, .T. ) ;
#8341=EDGE_LOOP ( 'NONE', ( #24396, #31158, #25510, #3677 ) ) ;
#8423=CARTESIAN_POINT ( 'NONE',  ( 109.3993806922052698, 20.31298924473501444, 2.334455007174201402 ) ) ;
#8479=CYLINDRICAL_SURFACE ( 'NONE', #19945, 303.6457063863960002 ) ;
#8491=B_SPLINE_CURVE_WITH_KNOTS ( 'NONE', 3,
 ( #2864, #21697, #8827, #32410, #1327, #8971 ),
 .UNSPECIFIED., .F., .F.,
 ( 4, 2, 4 ),
 ( 0.000000000000000000, 0.0009761896101137411321, 0.001952379220227482264 ),
 .UNSPECIFIED. ) ;
#8581=VECTOR ( 'NONE', #28695, 1000.000000000000114 ) ;
#8590=VERTEX_POINT ( 'NONE', #14595 ) ;
#8594=ORIENTED_EDGE ( 'NONE', *, *, #20802, .F. ) ;
#8609=AXIS2_PLACEMENT_3D ( 'NONE', #16763, #29291, #6377 ) ;
#8686=VERTEX_POINT ( 'NONE', #4733 ) ;
#8710=CIRCLE ( 'NONE', #6045, 301.6269746700523910 ) ;
#8735=ADVANCED_FACE ( 'NONE', ( #30975 ), #25224, .T. ) ;
#8742=EDGE_LOOP ( 'NONE', ( #12504, #5922, #18481, #343 ) ) ;
#8827=CARTESIAN_POINT ( 'NONE',  ( 108.5974656045667075, 15.84760961618085062, 1.739510335802044727 ) ) ;
#8840=DIRECTION ( 'NONE',  ( 0.04852105321274754329, -0.4695180821586618092, 0.8815886103626667802 ) ) ;
#8865=ADVANCED_FACE ( 'NONE', ( #15581 ), #22029, .T. ) ;
#8885=VERTEX_POINT ( 'NONE', #21259 ) ;
#8898=DIRECTION ( 'NONE',  ( -0.000000000000000000, -0.000000000000000000, -1.000000000000000000 ) ) ;
#8937=EDGE_CURVE ( 'NONE', #18451, #30629, #27375, .T. ) ;
#8963=ADVANCED_FACE ( 'NONE', ( #18742, #13866 ), #11213, .T. ) ;
#8971=CARTESIAN_POINT ( 'NONE',  ( 108.5619817448483531, 15.65002148400673754, 0.4463807625373211185 ) ) ;
#9020=CARTESIAN_POINT ( 'NONE',  ( 56.97280603064898941, -277.2763395528616002, -2.806473568333519353 ) ) ;
#9036=EDGE_LOOP ( 'NONE', ( #24774, #21737, #24214, #33005 ) ) ;
#9074=ORIENTED_EDGE ( 'NONE', *, *, #31084, .F. ) ;
#9084=DIRECTION ( 'NONE',  ( -0.000000000000000000, -0.000000000000000000, -1.000000000000000000 ) ) ;
#9126=DIRECTION ( 'NONE',  ( -0.1027947991993878318, 0.9947025833170222153, 0.000000000000000000 ) ) ;
#9143=CIRCLE ( 'NONE', #13417, 4.000000000000000000 ) ;
#9167=DIRECTION ( 'NONE',  ( -0.000000000000000000, -0.000000000000000000, -1.000000000000000000 ) ) ;
#9264=CARTESIAN_POINT ( 'NONE',  ( 56.97280603064898941, -277.2763395528616002, 2.334455007174216057 ) ) ;
#9286=ORIENTED_EDGE ( 'NONE', *, *, #2545, .T. ) ;
#9310=ADVANCED_FACE ( 'NONE', ( #21556 ), #20474, .T. ) ;
#9325=VERTEX_POINT ( 'NONE', #3177 ) ;
#9371=CARTESIAN_POINT ( 'NONE',  ( 56.97280603064898941, -277.2763395528616002, -0.4463807625373608645 ) ) ;
#9432=DIRECTION ( 'NONE',  ( -1.000000000000000000, 0.000000000000000000, 0.000000000000000000 ) ) ;
#9466=ORIENTED_EDGE ( 'NONE', *, *, #25932, .F. ) ;
#9488=EDGE_CURVE ( 'NONE', #31265, #28329, #12757, .T. ) ;
#9553=CARTESIAN_POINT ( 'NONE',  ( 26.13024263984371842, 21.17433810686647533, -4.621439243524461560 ) ) ;
#9617=DIRECTION ( 'NONE',  ( 1.000000000000000000, 0.000000000000000000, 0.000000000000000000 ) ) ;
#9651=DIRECTION ( 'NONE',  ( -0.1027947991993878041, 0.9947025833170221043, 0.000000000000000000 ) ) ;
#9676=CARTESIAN_POINT ( 'NONE',  ( 110.0070906499164352, 18.03948353657134263, 4.621439243524390506 ) ) ;
#9686=APPLICATION_CONTEXT ( 'configuration controlled 3d designs of mechanical parts and assemblies' ) ;
#9714=TOROIDAL_SURFACE ( 'NONE', #4908, 298.6457063863958865, 4.000000000000000888 ) ;
#9736=DIRECTION ( 'NONE',  ( -1.000000000000000000, 0.000000000000000000, 0.000000000000000000 ) ) ;
#9823=EDGE_CURVE ( 'NONE', #8686, #21913, #18339, .T. ) ;
#9863=DIRECTION ( 'NONE',  ( 0.1767573132311704154, 0.9842544651762052954, 0.000000000000000000 ) ) ;
#9877=ORIENTED_EDGE ( 'NONE', *, *, #14637, .F. ) ;
#9908=CARTESIAN_POINT ( 'NONE',  ( 109.3697760341437970, 14.49066428361112813, 0.4463807625373157340 ) ) ;
#9926=VERTEX_POINT ( 'NONE', #5395 ) ;
#9961=MANIFOLD_SOLID_BREP ( 'Shell1', #4414 ) ;
#9964=DIRECTION ( 'NONE',  ( 0.9947025833170223263, 0.1027947991993880261, 0.000000000000000000 ) ) ;
#10000=DIRECTION ( 'NONE',  ( 0.1767573132311711093, 0.9842544651762052954, 0.000000000000000000 ) ) ;
#10111=EDGE_LOOP ( 'NONE', ( #14561, #13120, #31791, #24702 ) ) ;
#10132=AXIS2_PLACEMENT_3D ( 'NONE', #29131, #5737, #15600 ) ;
#10156=CARTESIAN_POINT ( 'NONE',  ( 109.0479424394436734, 18.35604238244625819, -5.421472302580672142 ) ) ;
#10179=EDGE_CURVE ( 'NONE', #27014, #4554, #4927, .T. ) ;
#10181=CIRCLE ( 'NONE', #4846, 5.000000000000001776 ) ;
#10195=ORIENTED_EDGE ( 'NONE', *, *, #24583, .F. ) ;
#10260=AXIS2_PLACEMENT_3D ( 'NONE', #31908, #6469, #11014 ) ;
#10267=EDGE_CURVE ( 'NONE', #16936, #16263, #26280, .T. ) ;
#10270=ADVANCED_FACE ( 'NONE', ( #1885 ), #21909, .T. ) ;
#10347=CARTESIAN_POINT ( 'NONE',  ( 109.0732318695909129, 18.49686390823877957, -5.382000293758435028 ) ) ;
#10378=EDGE_CURVE ( 'NONE', #2795, #8885, #24655, .T. ) ;
#10387=ORIENTED_EDGE ( 'NONE', *, *, #3641, .T. ) ;
#10418=CARTESIAN_POINT ( 'NONE',  ( 56.97280603064898941, -277.2763395528616002, -4.621439243524461560 ) ) ;
#10427=CARTESIAN_POINT ( 'NONE',  ( 108.8978791464556508, 17.52043075494136204, -4.999054092451819642 ) ) ;
#10437=DIRECTION ( 'NONE',  ( -0.1027947991993878318, 0.9947025833170222153, 0.000000000000000000 ) ) ;
#10455=CARTESIAN_POINT ( 'NONE',  ( 108.6457025336241031, 16.11621187055573046, 2.334455007174216057 ) ) ;
#10490=DIRECTION ( 'NONE',  ( -0.000000000000000000, -0.000000000000000000, -1.000000000000000000 ) ) ;
#10497=ORIENTED_EDGE ( 'NONE', *, *, #15933, .F. ) ;
#10597=DIRECTION ( 'NONE',  ( -1.000000000000000000, 0.000000000000000000, 0.000000000000000000 ) ) ;
#10715=DIRECTION ( 'NONE',  ( 1.000000000000000000, 0.000000000000000000, 0.000000000000000000 ) ) ;
#10831=CONICAL_SURFACE ( 'NONE', #28970, 303.0536494382092769, 0.4915790642873723582 ) ;
#10852=EDGE_LOOP ( 'NONE', ( #19133, #10497, #10961, #25665 ) ) ;
#10961=ORIENTED_EDGE ( 'NONE', *, *, #3047, .F. ) ;
#10982=CARTESIAN_POINT ( 'NONE',  ( 26.44001828968095680, 18.17676778675652471, 2.806473568333413660 ) ) ;
#11014=DIRECTION ( 'NONE',  ( -1.000000000000000000, 0.000000000000000000, 0.000000000000000000 ) ) ;
#11041=EDGE_CURVE ( 'NONE', #21569, #7000, #3768, .T. ) ;
#11094=ADVANCED_FACE ( 'NONE', ( #479 ), #8479, .T. ) ;
#11117=DIRECTION ( 'NONE',  ( -1.000000000000000000, 0.000000000000000000, 0.000000000000000000 ) ) ;
#11133=VERTEX_POINT ( 'NONE', #29068 ) ;
#11141=VERTEX_POINT ( 'NONE', #29722 ) ;
#11151=CARTESIAN_POINT ( 'NONE',  ( 109.3153218317886513, 19.84491634189289400, 3.222654707407430319 ) ) ;
#11192=TOROIDAL_SURFACE ( 'NONE', #4256, 301.4345239564033250, 5.000000000000000888 ) ;
#11213=PLANE ( 'NONE',  #8169 ) ;
#11216=EDGE_CURVE ( 'NONE', #16936, #18451, #3807, .T. ) ;
#11244=EDGE_CURVE ( 'NONE', #24728, #29938, #7640, .T. ) ;
#11259=EDGE_CURVE ( 'NONE', #4825, #21913, #33048, .T. ) ;
#11402=DIRECTION ( 'NONE',  ( 0.000000000000000000, 0.000000000000000000, 1.000000000000000000 ) ) ;
#11428=CARTESIAN_POINT ( 'NONE',  ( 56.97280603064898941, -277.2763395528616002, -0.4463807625373771293 ) ) ;
#11560=VERTEX_POINT ( 'NONE', #121 ) ;
#11606=CARTESIAN_POINT ( 'NONE',  ( 25.75960661490314507, 24.76082900280849586, -0.4463807625373413246 ) ) ;
#11619=CARTESIAN_POINT ( 'NONE',  ( 109.1472041058641196, 18.90877050785844204, 4.999054092451761022 ) ) ;
#11686=ORIENTED_EDGE ( 'NONE', *, *, #9488, .F. ) ;
#11741=CARTESIAN_POINT ( 'NONE',  ( 108.5619817448483531, 15.65002148400673754, 0.4463807625373211185 ) ) ;
#11836=CARTESIAN_POINT ( 'NONE',  ( 109.1169603330106526, 18.74036124698735151, 5.233955722116973241 ) ) ;
#11914=VECTOR ( 'NONE', #31564, 1000.000000000000000 ) ;
#11939=AXIS2_PLACEMENT_3D ( 'NONE', #16086, #23795, #21284 ) ;
#11994=CARTESIAN_POINT ( 'NONE',  ( 56.97280603064898941, -277.2763395528616002, 0.000000000000000000 ) ) ;
#12060=CARTESIAN_POINT ( 'NONE',  ( 109.2693081351234241, 19.58869392272333343, 0.4463807625373348298 ) ) ;
#12066=ORIENTED_EDGE ( 'NONE', *, *, #5328, .F. ) ;
#12074=ORIENTED_EDGE ( 'NONE', *, *, #3476, .T. ) ;
#12100=ORIENTED_EDGE ( 'NONE', *, *, #31328, .T. ) ;
#12111=B_SPLINE_CURVE_WITH_KNOTS ( 'NONE', 3,
 ( #20212, #22727, #22555, #5167, #33079, #10156, #10347, #22876, #30408, #2504 ),
 .UNSPECIFIED., .F., .F.,
 ( 4, 2, 2, 2, 4 ),
 ( 0.000000000000000000, 0.0004294301528457186799, 0.0008588603056914373597, 0.001288290458537156040, 0.001717720611382874719 ),
 .UNSPECIFIED. ) ;
#12118=FACE_OUTER_BOUND ( 'NONE', #27101, .T. ) ;
#12178=DIRECTION ( 'NONE',  ( -1.000000000000000000, 0.000000000000000000, 0.000000000000000000 ) ) ;
#12199=EDGE_CURVE ( 'NONE', #17109, #19335, #19412, .T. ) ;
#12267=DIRECTION ( 'NONE',  ( 0.000000000000000000, 0.000000000000000000, -1.000000000000000000 ) ) ;
#12315=EDGE_LOOP ( 'NONE', ( #3918, #17529, #13657, #4704 ) ) ;
#12317=EDGE_LOOP ( 'NONE', ( #21364, #14107, #2895, #4003 ) ) ;
#12385=EDGE_LOOP ( 'NONE', ( #8314, #8170, #2982, #28382 ) ) ;
#12386=VECTOR ( 'NONE', #5208, 1000.000000000000000 ) ;
#12417=ORIENTED_EDGE ( 'NONE', *, *, #1034, .T. ) ;
#12456=AXIS2_PLACEMENT_3D ( 'NONE', #6625, #32035, #3969 ) ;
#12481=FACE_OUTER_BOUND ( 'NONE', #1561, .T. ) ;
#12493=DIRECTION ( 'NONE',  ( 0.08343273266574550984, 0.4645863764670127849, -0.8815886103626664472 ) ) ;
#12504=ORIENTED_EDGE ( 'NONE', *, *, #31328, .F. ) ;
#12580=DIRECTION ( 'NONE',  ( 0.1027947991993887200, -0.9947025833170221043, 1.084202172485531452E-15 ) ) ;
#12749=ORIENTED_EDGE ( 'NONE', *, *, #25835, .F. ) ;
#12757=B_SPLINE_CURVE_WITH_KNOTS ( 'NONE', 3,
 ( #19543, #19383, #6667, #4322, #14499, #29740 ),
 .UNSPECIFIED., .F., .F.,
 ( 4, 2, 4 ),
 ( 0.000000000000000000, 0.0009761895971467555739, 0.001952379194293511148 ),
 .UNSPECIFIED. ) ;
#12842=CARTESIAN_POINT ( 'NONE',  ( 108.5619817448483815, 15.65002148400668247, -0.7764623266635863885 ) ) ;
#12913=AXIS2_PLACEMENT_3D ( 'NONE', #28717, #30768, #7839 ) ;
#12957=CARTESIAN_POINT ( 'NONE',  ( 108.8138202772576903, 17.05235780320132122, 4.110854392070696584 ) ) ;
#12961=CIRCLE ( 'NONE', #25792, 297.4345239564032681 ) ;
#12971=CONICAL_SURFACE ( 'NONE', #24177, 301.6269746700523342, 0.4915790642873871796 ) ;
#13120=ORIENTED_EDGE ( 'NONE', *, *, #917, .F. ) ;
#13182=CARTESIAN_POINT ( 'NONE',  ( 108.5690947754410018, 15.68962964501444546, -1.099690591032340459 ) ) ;
#13200=ORIENTED_EDGE ( 'NONE', *, *, #10378, .F. ) ;
#13348=ORIENTED_EDGE ( 'NONE', *, *, #526, .F. ) ;
#13350=DIRECTION ( 'NONE',  ( -0.1027947991993877902, 0.9947025833170222153, 0.000000000000000000 ) ) ;
#13417=AXIS2_PLACEMENT_3D ( 'NONE', #18295, #31006, #30705 ) ;
#13428=CARTESIAN_POINT ( 'NONE',  ( 109.4831014662948974, 20.77917954950586577, -0.4463807625373443777 ) ) ;
#13432=ORIENTED_EDGE ( 'NONE', *, *, #14781, .T. ) ;
#13443=AXIS2_PLACEMENT_3D ( 'NONE', #5710, #15891, #3204 ) ;
#13444=CIRCLE ( 'NONE', #32163, 0.7999999999999800604 ) ;
#13450=CONICAL_SURFACE ( 'NONE', #2796, 298.4532556727467068, 0.4915790642873356098 ) ;
#13525=VECTOR ( 'NONE', #11402, 1000.000000000000000 ) ;
#13561=DIRECTION ( 'NONE',  ( 0.1027947991993880122, -0.9947025833170222153, 0.000000000000000000 ) ) ;
#13634=CARTESIAN_POINT ( 'NONE',  ( 26.20274081918672593, 20.47280333234597194, -4.999054092451830300 ) ) ;
#13657=ORIENTED_EDGE ( 'NONE', *, *, #692, .F. ) ;
#13836=CARTESIAN_POINT ( 'NONE',  ( 56.97280603064898941, -277.2763395528616002, 2.806473568333438084 ) ) ;
#13866=FACE_BOUND ( 'NONE', #21923, .T. ) ;
#13868=ORIENTED_EDGE ( 'NONE', *, *, #17940, .T. ) ;
#13934=ADVANCED_FACE ( 'NONE', ( #30053 ), #16596, .F. ) ;
#14106=ORIENTED_EDGE ( 'NONE', *, *, #16588, .T. ) ;
#14107=ORIENTED_EDGE ( 'NONE', *, *, #6133, .F. ) ;
#14112=CARTESIAN_POINT ( 'NONE',  ( 108.8138202772576903, 17.05235780320128569, -4.110854392070767638 ) ) ;
#14158=CARTESIAN_POINT ( 'NONE',  ( 25.96712173632212384, 22.75279134953752447, -5.471072653611070535 ) ) ;
#14182=DIRECTION ( 'NONE',  ( 0.1027947991993878873, -0.9947025833170223263, 2.669847849745554669E-15 ) ) ;
#14224=EDGE_LOOP ( 'NONE', ( #10387, #31858, #21755, #16279 ) ) ;
#14253=ORIENTED_EDGE ( 'NONE', *, *, #27663, .F. ) ;
#14363=CARTESIAN_POINT ( 'NONE',  ( 25.98690466878746008, 22.56136012750956965, -0.4463807625373771293 ) ) ;
#14403=CARTESIAN_POINT ( 'NONE',  ( 56.97280603064898941, -277.2763395528616002, 4.999054092451758358 ) ) ;
#14415=AXIS2_PLACEMENT_3D ( 'NONE', #16832, #1129, #31741 ) ;
#14499=CARTESIAN_POINT ( 'NONE',  ( 109.4831014662949116, 20.77917954950587998, -0.7764623179268941300 ) ) ;
#14504=TOROIDAL_SURFACE ( 'NONE', #12913, 298.6457063863958865, 4.000000000000000888 ) ;
#14561=ORIENTED_EDGE ( 'NONE', *, *, #692, .T. ) ;
#14595=CARTESIAN_POINT ( 'NONE',  ( 110.5397548702477764, 21.00556809464029939, -2.806473568333519353 ) ) ;
#14637=EDGE_CURVE ( 'NONE', #30629, #4825, #21949, .T. ) ;
#14678=CARTESIAN_POINT ( 'NONE',  ( 108.8978791464556508, 17.52043075494136204, 4.999054092451758358 ) ) ;
#14685=EDGE_CURVE ( 'NONE', #2615, #17109, #26873, .T. ) ;
#14781=EDGE_CURVE ( 'NONE', #2615, #11560, #2231, .T. ) ;
#14796=CARTESIAN_POINT ( 'NONE',  ( 0.000000000000000000, 0.000000000000000000, 0.000000000000000000 ) ) ;
#14812=FACE_OUTER_BOUND ( 'NONE', #8341, .T. ) ;
#14854=ORIENTED_EDGE ( 'NONE', *, *, #16588, .F. ) ;
#14863=CARTESIAN_POINT ( 'NONE',  ( 109.4744264295851082, 15.07339897850245158, 2.806473568333413660 ) ) ;
#14911=DIRECTION ( 'NONE',  ( -0.000000000000000000, -0.000000000000000000, -1.000000000000000000 ) ) ;
#14927=DIRECTION ( 'NONE',  ( 0.000000000000000000, 0.000000000000000000, -1.000000000000000000 ) ) ;
#14928=CARTESIAN_POINT ( 'NONE',  ( 26.34939556550225248, 19.05368625490715928, 2.334455007174210728 ) ) ;
#14941=DIRECTION ( 'NONE',  ( -0.000000000000000000, -0.000000000000000000, -1.000000000000000000 ) ) ;
#14972=DIRECTION ( 'NONE',  ( 0.1027947991993878873, -0.9947025833170223263, 3.550762114890027021E-15 ) ) ;
#14973=LINE ( 'NONE', #2310, #22481 ) ;
#14986=PLANE ( 'NONE',  #16729 ) ;
#14990=ORIENTED_EDGE ( 'NONE', *, *, #11259, .T. ) ;
#15000=EDGE_CURVE ( 'NONE', #24269, #28814, #28381, .T. ) ;
#15077=DIRECTION ( 'NONE',  ( -0.000000000000000000, -0.000000000000000000, -1.000000000000000000 ) ) ;
#15120=DIRECTION ( 'NONE',  ( -0.000000000000000000, -0.000000000000000000, -1.000000000000000000 ) ) ;
#15164=DIRECTION ( 'NONE',  ( 0.9947025833170223263, 0.1027947991993880261, -0.000000000000000000 ) ) ;
#15165=CARTESIAN_POINT ( 'NONE',  ( 108.6457025336241031, 16.11621187055573046, 2.334455007174216057 ) ) ;
#15214=ADVANCED_FACE ( 'NONE', ( #18916 ), #13450, .F. ) ;
#15255=VERTEX_POINT ( 'NONE', #6515 ) ;
#15277=CARTESIAN_POINT ( 'NONE',  ( 56.97280603064898941, -277.2763395528616002, -2.334455007174250696 ) ) ;
#15281=DIRECTION ( 'NONE',  ( -0.000000000000000000, -0.000000000000000000, -1.000000000000000000 ) ) ;
#15298=EDGE_CURVE ( 'NONE', #2614, #17163, #22540, .T. ) ;
#15314=DIRECTION ( 'NONE',  ( 0.000000000000000000, 0.000000000000000000, 1.000000000000000000 ) ) ;
#15400=DIRECTION ( 'NONE',  ( -0.1027947991993876653, 0.9947025833170222153, 0.000000000000000000 ) ) ;
#15422=ORIENTED_EDGE ( 'NONE', *, *, #31861, .F. ) ;
#15440=CARTESIAN_POINT ( 'NONE',  ( 109.4269204153489454, 20.46634128985479961, 2.043459224939188967 ) ) ;
#15487=CIRCLE ( 'NONE', #1061, 297.0265809045899346 ) ;
#15530=AXIS2_PLACEMENT_3D ( 'NONE', #22664, #78, #27654 ) ;
#15544=CARTESIAN_POINT ( 'NONE',  ( 26.39808386558502562, 18.58254979424150832, 0.4463807625373201193 ) ) ;
#15581=FACE_OUTER_BOUND ( 'NONE', #30972, .T. ) ;
#15596=CIRCLE ( 'NONE', #17192, 298.4532556727467636 ) ;
#15600=DIRECTION ( 'NONE',  ( -1.000000000000000000, 0.000000000000000000, 0.000000000000000000 ) ) ;
#15615=AXIS2_PLACEMENT_3D ( 'NONE', #22266, #32477, #30149 ) ;
#15662=DIRECTION ( 'NONE',  ( -0.1027947991993877763, 0.9947025833170223263, 0.000000000000000000 ) ) ;
#15681=LINE ( 'NONE', #3003, #5010 ) ;
#15693=TOROIDAL_SURFACE ( 'NONE', #27963, 300.0401151713995773, 0.7999999999999787281 ) ;
#15702=DIRECTION ( 'NONE',  ( -1.000000000000000000, 0.000000000000000000, 0.000000000000000000 ) ) ;
#15820=VERTEX_POINT ( 'NONE', #307 ) ;
#15877=VERTEX_POINT ( 'NONE', #15165 ) ;
#15884=LINE ( 'NONE', #23265, #12386 ) ;
#15891=DIRECTION ( 'NONE',  ( 0.9947025833170223263, 0.1027947991993880261, -0.000000000000000000 ) ) ;
#15933=EDGE_CURVE ( 'NONE', #11141, #30909, #14973, .T. ) ;
#15967=EDGE_CURVE ( 'NONE', #17163, #25473, #3472, .T. ) ;
#15969=DIRECTION ( 'NONE',  ( -0.000000000000000000, -0.000000000000000000, -1.000000000000000000 ) ) ;
#16057=CIRCLE ( 'NONE', #17143, 302.1720608278465079 ) ;
#16068=ORIENTED_EDGE ( 'NONE', *, *, #11259, .F. ) ;
#16086=CARTESIAN_POINT ( 'NONE',  ( 56.97280603064898941, -277.2763395528616002, -4.999054092451819642 ) ) ;
#16101=ADVANCED_FACE ( 'NONE', ( #7926 ), #29956, .F. ) ;
#16113=AXIS2_PLACEMENT_3D ( 'NONE', #4371, #29943, #30137 ) ;
#16263=VERTEX_POINT ( 'NONE', #6522 ) ;
#16271=FACE_OUTER_BOUND ( 'NONE', #22985, .T. ) ;
#16279=ORIENTED_EDGE ( 'NONE', *, *, #17906, .T. ) ;
#16439=ORIENTED_EDGE ( 'NONE', *, *, #32453, .F. ) ;
#16448=CARTESIAN_POINT ( 'NONE',  ( 56.97280603064898941, -277.2763395528616002, 0.4463807625373348298 ) ) ;
#16577=ORIENTED_EDGE ( 'NONE', *, *, #25932, .T. ) ;
#16583=DESIGN_CONTEXT ( 'detailed design', #18239, 'design' ) ;
#16588=EDGE_CURVE ( 'NONE', #29938, #11560, #5405, .T. ) ;
#16596=CONICAL_SURFACE ( 'NONE', #2740, 297.0265809045899346, 0.4915790642873721361 ) ;
#16692=ORIENTED_EDGE ( 'NONE', *, *, #3476, .F. ) ;
#16706=ADVANCED_FACE ( 'NONE', ( #31755 ), #24083, .T. ) ;
#16729=AXIS2_PLACEMENT_3D ( 'NONE', #27882, #30396, #7975 ) ;
#16749=AXIS2_PLACEMENT_3D ( 'NONE', #11994, #24195, #1319 ) ;
#16763=CARTESIAN_POINT ( 'NONE',  ( 25.98690466878746008, 22.56136012750956965, 0.4463807625373348298 ) ) ;
#16832=CARTESIAN_POINT ( 'NONE',  ( 110.0070906499164352, 18.03948353657134263, -4.621439243524461560 ) ) ;
#16837=CARTESIAN_POINT ( 'NONE',  ( 56.97280603064898941, -277.2763395528616002, -0.4463807625373402699 ) ) ;
#16936=VERTEX_POINT ( 'NONE', #19371 ) ;
#16971=ORIENTED_EDGE ( 'NONE', *, *, #14637, .T. ) ;
#17109=VERTEX_POINT ( 'NONE', #13634 ) ;
#17119=EDGE_CURVE ( 'NONE', #4621, #24728, #7564, .T. ) ;
#17120=AXIS2_PLACEMENT_3D ( 'NONE', #5132, #9964, #1967 ) ;
#17138=DIRECTION ( 'NONE',  ( -0.000000000000000000, -0.000000000000000000, -1.000000000000000000 ) ) ;
#17143=AXIS2_PLACEMENT_3D ( 'NONE', #7780, #15120, #10597 ) ;
#17157=EDGE_CURVE ( 'NONE', #11133, #2614, #26664, .T. ) ;
#17158=DIRECTION ( 'NONE',  ( -0.000000000000000000, -0.000000000000000000, -1.000000000000000000 ) ) ;
#17163=VERTEX_POINT ( 'NONE', #1290 ) ;
#17178=ORIENTED_EDGE ( 'NONE', *, *, #1034, .F. ) ;
#17186=CARTESIAN_POINT ( 'NONE',  ( 25.91108971418532292, 23.29498995882573098, 2.334455007174183194 ) ) ;
#17192=AXIS2_PLACEMENT_3D ( 'NONE', #3235, #7331, #25038 ) ;
#17243=DIRECTION ( 'NONE',  ( -0.9842544651762054064, 0.1767573132311699990, 0.000000000000000000 ) ) ;
#17247=CIRCLE ( 'NONE', #24613, 1.799999999999977396 ) ;
#17331=DIRECTION ( 'NONE',  ( 0.9947025833170223263, 0.1027947991993880261, -0.000000000000000000 ) ) ;
#17362=CARTESIAN_POINT ( 'NONE',  ( 108.9718513837279517, 17.93233736012435742, 5.382000289407169902 ) ) ;
#17377=ORIENTED_EDGE ( 'NONE', *, *, #11216, .F. ) ;
#17402=LINE ( 'NONE', #25068, #24154 ) ;
#17493=CARTESIAN_POINT ( 'NONE',  ( 26.27358061090003361, 19.78731608622335969, 0.4463807625373084065 ) ) ;
#17507=CARTESIAN_POINT ( 'NONE',  ( 109.1350892575554070, 18.84131025218471578, 5.127064441657748439 ) ) ;
#17529=ORIENTED_EDGE ( 'NONE', *, *, #17157, .F. ) ;
#17549=ADVANCED_FACE ( 'NONE', ( #27268 ), #3879, .F. ) ;
#17596=ORIENTED_EDGE ( 'NONE', *, *, #6133, .T. ) ;
#17633=ORIENTED_EDGE ( 'NONE', *, *, #17931, .F. ) ;
#17707=VECTOR ( 'NONE', #6645, 1000.000000000000114 ) ;
#17713=AXIS2_PLACEMENT_3D ( 'NONE', #14403, #14911, #4741 ) ;
#17723=AXIS2_PLACEMENT_3D ( 'NONE', #14363, #2033, #24413 ) ;
#17727=VECTOR ( 'NONE', #4809, 999.9999999999998863 ) ;
#17730=AXIS2_PLACEMENT_3D ( 'NONE', #25450, #17932, #10715 ) ;
#17765=TOROIDAL_SURFACE ( 'NONE', #26326, 301.4345239564033250, 4.000000000000000888 ) ;
#17844=CIRCLE ( 'NONE', #21564, 303.0536494382092769 ) ;
#17906=EDGE_CURVE ( 'NONE', #9926, #22465, #23599, .T. ) ;
#17910=LINE ( 'NONE', #15544, #1787 ) ;
#17931=EDGE_CURVE ( 'NONE', #17109, #2795, #13444, .T. ) ;
#17932=DIRECTION ( 'NONE',  ( 0.000000000000000000, 0.000000000000000000, 1.000000000000000000 ) ) ;
#17940=EDGE_CURVE ( 'NONE', #9325, #29938, #12961, .T. ) ;
#17955=VERTEX_POINT ( 'NONE', #9908 ) ;
#17986=( NAMED_UNIT ( * ) PLANE_ANGLE_UNIT ( ) SI_UNIT ( $, .RADIAN. ) );
#17993=ORIENTED_EDGE ( 'NONE', *, *, #4705, .T. ) ;
#17994=CARTESIAN_POINT ( 'NONE',  ( 26.44001828968094259, 18.17676778675653537, -2.806473568333505586 ) ) ;
#18061=ORIENTED_EDGE ( 'NONE', *, *, #32263, .T. ) ;
#18071=ORIENTED_EDGE ( 'NONE', *, *, #5328, .T. ) ;
#18190=CARTESIAN_POINT ( 'NONE',  ( 109.1472041058641196, 18.90877050785844204, 4.999054092451761022 ) ) ;
#18230=AXIS2_PLACEMENT_3D ( 'NONE', #21067, #31267, #28888 ) ;
#18239=APPLICATION_CONTEXT ( 'configuration controlled 3d designs of mechanical parts and assemblies' ) ;
#18253=VERTEX_POINT ( 'NONE', #30934 ) ;
#18281=ORIENTED_EDGE ( 'NONE', *, *, #4425, .F. ) ;
#18295=CARTESIAN_POINT ( 'NONE',  ( 25.98690466878739613, 22.56136012750964426, 0.4463807625373348298 ) ) ;
#18307=EDGE_CURVE ( 'NONE', #25473, #17955, #26848, .T. ) ;
#18339=CIRCLE ( 'NONE', #12456, 303.6457063863959434 ) ;
#18390=CARTESIAN_POINT ( 'NONE',  ( 108.6457025336241031, 16.11621187055573046, -2.334455007174250696 ) ) ;
#18449=FACE_OUTER_BOUND ( 'NONE', #4500, .T. ) ;
#18450=EDGE_LOOP ( 'NONE', ( #19791, #16068, #9877, #31731 ) ) ;
#18451=VERTEX_POINT ( 'NONE', #19040 ) ;
#18481=ORIENTED_EDGE ( 'NONE', *, *, #29402, .T. ) ;
#18496=ORIENTED_EDGE ( 'NONE', *, *, #20488, .T. ) ;
#18584=DIRECTION ( 'NONE',  ( 0.9947025833170223263, 0.1027947991993880261, 0.000000000000000000 ) ) ;
#18635=ORIENTED_EDGE ( 'NONE', *, *, #17157, .T. ) ;
#18697=AXIS2_PLACEMENT_3D ( 'NONE', #5504, #23526, #3014 ) ;
#18731=CIRCLE ( 'NONE', #26721, 4.000000000000000000 ) ;
#18742=FACE_OUTER_BOUND ( 'NONE', #23255, .T. ) ;
#18789=EDGE_CURVE ( 'NONE', #389, #9926, #27054, .T. ) ;
#18797=EDGE_LOOP ( 'NONE', ( #16971, #7765, #27494, #24419 ) ) ;
#18861=AXIS2_PLACEMENT_3D ( 'NONE', #31108, #24031, #1157 ) ;
#18871=VERTEX_POINT ( 'NONE', #17186 ) ;
#18916=FACE_OUTER_BOUND ( 'NONE', #486, .T. ) ;
#18926=EDGE_CURVE ( 'NONE', #9926, #2614, #8710, .T. ) ;
#18932=ORIENTED_EDGE ( 'NONE', *, *, #526, .T. ) ;
#18935=LINE ( 'NONE', #21752, #13525 ) ;
#18999=CARTESIAN_POINT ( 'NONE',  ( 110.2535626002996310, 19.41193660949215882, -0.4463807625373771293 ) ) ;
#19040=CARTESIAN_POINT ( 'NONE',  ( 25.82046699000660439, 24.17190842697640818, -2.806473568333519353 ) ) ;
#19095=CARTESIAN_POINT ( 'NONE',  ( 56.97280603064898941, -277.2763395528616002, -0.4463807625373443777 ) ) ;
#19133=ORIENTED_EDGE ( 'NONE', *, *, #5068, .T. ) ;
#19172=ORIENTED_EDGE ( 'NONE', *, *, #11216, .T. ) ;
#19193=VECTOR ( 'NONE', #7919, 999.9999999999998863 ) ;
#19238=VECTOR ( 'NONE', #3945, 1000.000000000000000 ) ;
#19267=EDGE_CURVE ( 'NONE', #19723, #15877, #2847, .T. ) ;
#19335=VERTEX_POINT ( 'NONE', #29490 ) ;
#19371=CARTESIAN_POINT ( 'NONE',  ( 25.96712173632212384, 22.75279134953750670, -5.471072653611063430 ) ) ;
#19378=ORIENTED_EDGE ( 'NONE', *, *, #29402, .F. ) ;
#19383=CARTESIAN_POINT ( 'NONE',  ( 109.4269204146996515, 20.46634128623930948, -2.043459231800118125 ) ) ;
#19412=CIRCLE ( 'NONE', #11939, 299.3348442831094758 ) ;
#19485=DIRECTION ( 'NONE',  ( -0.000000000000000000, -0.000000000000000000, -1.000000000000000000 ) ) ;
#19495=ADVANCED_FACE ( 'NONE', ( #20281 ), #15693, .F. ) ;
#19541=LINE ( 'NONE', #4652, #17727 ) ;
#19543=CARTESIAN_POINT ( 'NONE',  ( 109.3993806922052840, 20.31298924473512457, -2.334455007174283558 ) ) ;
#19557=EDGE_CURVE ( 'NONE', #15820, #4283, #18935, .T. ) ;
#19581=DIRECTION ( 'NONE',  ( -0.000000000000000000, -0.000000000000000000, -1.000000000000000000 ) ) ;
#19586=CARTESIAN_POINT ( 'NONE',  ( 108.8978791464556508, 17.52043075494136204, 4.999054092451758358 ) ) ;
#19607=ORIENTED_EDGE ( 'NONE', *, *, #917, .T. ) ;
#19704=ORIENTED_EDGE ( 'NONE', *, *, #10267, .T. ) ;
#19723=VERTEX_POINT ( 'NONE', #19586 ) ;
#19791=ORIENTED_EDGE ( 'NONE', *, *, #9823, .T. ) ;
#19827=ORIENTED_EDGE ( 'NONE', *, *, #31553, .T. ) ;
#19833=DIRECTION ( 'NONE',  ( -0.000000000000000000, -0.000000000000000000, -1.000000000000000000 ) ) ;
#19837=VECTOR ( 'NONE', #12267, 1000.000000000000000 ) ;
#19852=CARTESIAN_POINT ( 'NONE',  ( 56.97280603064898941, -277.2763395528616002, 0.000000000000000000 ) ) ;
#19872=AXIS2_PLACEMENT_3D ( 'NONE', #9676, #4176, #9863 ) ;
#19909=CARTESIAN_POINT ( 'NONE',  ( 26.29336354336545867, 19.59588486419530184, 5.471072653610988823 ) ) ;
#19945=AXIS2_PLACEMENT_3D ( 'NONE', #28721, #335, #15702 ) ;
#19986=ORIENTED_EDGE ( 'NONE', *, *, #8937, .F. ) ;
#20019=CARTESIAN_POINT ( 'NONE',  ( 108.5619817448483531, 15.65002148400668247, -0.4463807625373593657 ) ) ;
#20177=DIRECTION ( 'NONE',  ( -1.000000000000000000, 0.000000000000000000, 0.000000000000000000 ) ) ;
#20199=FACE_OUTER_BOUND ( 'NONE', #21474, .T. ) ;
#20212=CARTESIAN_POINT ( 'NONE',  ( 108.8978791464556508, 17.52043075494136204, -4.999054092451819642 ) ) ;
#20275=CARTESIAN_POINT ( 'NONE',  ( 56.97280603064898941, -277.2763395528616002, 0.4463807625373084065 ) ) ;
#20281=FACE_OUTER_BOUND ( 'NONE', #32416, .T. ) ;
#20312=CARTESIAN_POINT ( 'NONE',  ( 109.4831014662949258, 20.77917954950597590, 0.4463807625372899768 ) ) ;
#20413=ADVANCED_FACE ( 'NONE', ( #18449 ), #895, .T. ) ;
#20417=CARTESIAN_POINT ( 'NONE',  ( 25.86240141410254978, 23.76612641949149562, 0.4463807625372899768 ) ) ;
#20474=TOROIDAL_SURFACE ( 'NONE', #18861, 298.6457063863958865, 5.000000000000000888 ) ;
#20488=EDGE_CURVE ( 'NONE', #8885, #31265, #5137, .T. ) ;
#20502=ORIENTED_EDGE ( 'NONE', *, *, #19267, .F. ) ;
#20632=ORIENTED_EDGE ( 'NONE', *, *, #15967, .T. ) ;
#20642=DIRECTION ( 'NONE',  ( 0.9947025833170223263, 0.1027947991993880261, 0.000000000000000000 ) ) ;
#20648=DIRECTION ( 'NONE',  ( -0.000000000000000000, -0.000000000000000000, -1.000000000000000000 ) ) ;
#20669=CARTESIAN_POINT ( 'NONE',  ( 56.97280603064898941, -277.2763395528616002, 0.4463807625372899768 ) ) ;
#20707=ORIENTED_EDGE ( 'NONE', *, *, #23525, .T. ) ;
#20777=DIRECTION ( 'NONE',  ( -0.000000000000000000, -0.000000000000000000, -1.000000000000000000 ) ) ;
#20802=EDGE_CURVE ( 'NONE', #30629, #8686, #26823, .T. ) ;
#20806=ORIENTED_EDGE ( 'NONE', *, *, #4705, .F. ) ;
#20854=ORIENTED_EDGE ( 'NONE', *, *, #7087, .F. ) ;
#20867=FACE_OUTER_BOUND ( 'NONE', #3993, .T. ) ;
#20912=CONICAL_SURFACE ( 'NONE', #25173, 297.9081695149525899, 0.4915790642873721361 ) ;
#20926=CIRCLE ( 'NONE', #17713, 299.3348442831094189 ) ;
#20934=AXIS2_PLACEMENT_3D ( 'NONE', #30027, #14941, #32215 ) ;
#21067=CARTESIAN_POINT ( 'NONE',  ( 56.97280603064898941, -277.2763395528616002, 4.621439243524390506 ) ) ;
#21095=ORIENTED_EDGE ( 'NONE', *, *, #11244, .T. ) ;
#21145=CARTESIAN_POINT ( 'NONE',  ( 109.4480141202987369, 20.58379936219382245, 1.732900863439792660 ) ) ;
#21259=CARTESIAN_POINT ( 'NONE',  ( 109.1472041058640912, 18.90877050785832836, -4.999054092451833853 ) ) ;
#21271=ORIENTED_EDGE ( 'NONE', *, *, #14781, .F. ) ;
#21284=DIRECTION ( 'NONE',  ( -1.000000000000000000, 0.000000000000000000, 0.000000000000000000 ) ) ;
#21314=FACE_OUTER_BOUND ( 'NONE', #9036, .T. ) ;
#21364=ORIENTED_EDGE ( 'NONE', *, *, #5326, .F. ) ;
#21405=CARTESIAN_POINT ( 'NONE',  ( 56.97280603064898941, -277.2763395528616002, 5.471072653610983494 ) ) ;
#21418=CARTESIAN_POINT ( 'NONE',  ( 25.98690466878746008, 22.56136012750956965, 0.4463807625373348298 ) ) ;
#21474=EDGE_LOOP ( 'NONE', ( #4160, #8295, #27886, #4682, #18071, #2574, #3563, #14990, #19607, #18635, #5180, #20632 ) ) ;
#21556=FACE_OUTER_BOUND ( 'NONE', #18797, .T. ) ;
#21564=AXIS2_PLACEMENT_3D ( 'NONE', #13836, #5694, #13350 ) ;
#21569=VERTEX_POINT ( 'NONE', #22231 ) ;
#21624=DIRECTION ( 'NONE',  ( -1.000000000000000000, 0.000000000000000000, 0.000000000000000000 ) ) ;
#21697=CARTESIAN_POINT ( 'NONE',  ( 108.6181628074316450, 15.96285980845909158, 2.043459238665831013 ) ) ;
#21737=ORIENTED_EDGE ( 'NONE', *, *, #32426, .F. ) ;
#21752=CARTESIAN_POINT ( 'NONE',  ( 25.86240141410256044, 23.76612641949138549, -0.4463807625373443777 ) ) ;
#21755=ORIENTED_EDGE ( 'NONE', *, *, #18926, .F. ) ;
#21826=DIRECTION ( 'NONE',  ( 1.000000000000000000, 0.000000000000000000, 0.000000000000000000 ) ) ;
#21909=PLANE ( 'NONE',  #4401 ) ;
#21913=VERTEX_POINT ( 'NONE', #24857 ) ;
#21923=EDGE_LOOP ( 'NONE', ( #2146, #20707, #18932, #26028, #33040, #4546, #27424, #29941, #24452, #12074, #17596, #16577 ) ) ;
#21949=CIRCLE ( 'NONE', #31068, 303.6457063863959434 ) ;
#22009=ADVANCED_FACE ( 'NONE', ( #14812 ), #2951, .F. ) ;
#22028=PRODUCT ( 'Part8_handle2Sleeve', 'Part8_handle2Sleeve', '', ( #22551 ) ) ;
#22029=TOROIDAL_SURFACE ( 'NONE', #162, 301.4345239564033250, 4.999999999999999112 ) ;
#22047=CARTESIAN_POINT ( 'NONE',  ( 108.9971408137216287, 18.07315888506168733, 5.421472300029551050 ) ) ;
#22196=DIRECTION ( 'NONE',  ( -0.000000000000000000, -0.000000000000000000, -1.000000000000000000 ) ) ;
#22207=EDGE_LOOP ( 'NONE', ( #19704, #12066, #3061, #19827 ) ) ;
#22231=CARTESIAN_POINT ( 'NONE',  ( 109.3993806922052698, 20.31298924473501444, 2.334455007174201402 ) ) ;
#22266=CARTESIAN_POINT ( 'NONE',  ( 56.97280603064898941, -277.2763395528616002, 2.334455007174208507 ) ) ;
#22404=ORIENTED_EDGE ( 'NONE', *, *, #10179, .F. ) ;
#22433=AXIS2_PLACEMENT_3D ( 'NONE', #19852, #22196, #29876 ) ;
#22450=EDGE_CURVE ( 'NONE', #8590, #4825, #10181, .T. ) ;
#22465=VERTEX_POINT ( 'NONE', #19909 ) ;
#22481=VECTOR ( 'NONE', #12493, 1000.000000000000000 ) ;
#22495=EDGE_CURVE ( 'NONE', #9325, #2615, #18731, .T. ) ;
#22540=CIRCLE ( 'NONE', #19872, 1.800000000000017142 ) ;
#22541=ADVANCED_FACE ( 'NONE', ( #32722 ), #31018, .T. ) ;
#22551=MECHANICAL_CONTEXT ( 'NONE', #9686, 'mechanical' ) ;
#22555=CARTESIAN_POINT ( 'NONE',  ( 108.9281229201717736, 17.68884002061582450, -5.233955718285084657 ) ) ;
#22557=CIRCLE ( 'NONE', #20934, 296.4345239564032113 ) ;
#22664=CARTESIAN_POINT ( 'NONE',  ( 56.97280603064898941, -277.2763395528616002, 4.621439243524390506 ) ) ;
#22727=CARTESIAN_POINT ( 'NONE',  ( 108.9099939952607627, 17.58789101337935179, -5.127064440218127572 ) ) ;
#22786=DIRECTION ( 'NONE',  ( -0.000000000000000000, -0.000000000000000000, -1.000000000000000000 ) ) ;
#22788=EDGE_LOOP ( 'NONE', ( #18061, #26718, #28968, #19172 ) ) ;
#22874=EDGE_CURVE ( 'NONE', #15877, #24728, #8491, .T. ) ;
#22876=CARTESIAN_POINT ( 'NONE',  ( 109.1168901022274724, 18.73997017427486256, -5.234450360147447689 ) ) ;
#22985=EDGE_LOOP ( 'NONE', ( #21271, #1323, #13868, #14106 ) ) ;
#23004=ORIENTED_EDGE ( 'NONE', *, *, #9488, .T. ) ;
#23030=AXIS2_PLACEMENT_3D ( 'NONE', #15277, #25988, #25827 ) ;
#23071=CIRCLE ( 'NONE', #30022, 300.7453860596897357 ) ;
#23105=ORIENTED_EDGE ( 'NONE', *, *, #11041, .F. ) ;
#23208=B_SPLINE_CURVE_WITH_KNOTS ( 'NONE', 3,
 ( #20312, #30522, #573, #21145, #15440, #8423 ),
 .UNSPECIFIED., .F., .F.,
 ( 4, 2, 4 ),
 ( 0.000000000000000000, 0.0009761895847327114973, 0.001952379169465422995 ),
 .UNSPECIFIED. ) ;
#23214=DIRECTION ( 'NONE',  ( -0.1027947991993878041, 0.9947025833170222153, 0.000000000000000000 ) ) ;
#23255=EDGE_LOOP ( 'NONE', ( #7405, #3193, #3183, #31094, #4748, #8594, #19986, #17377, #3689, #16439, #22404, #218 ) ) ;
#23265=CARTESIAN_POINT ( 'NONE',  ( 109.4831014662948974, 20.77917954950586577, -0.4463807625373443777 ) ) ;
#23286=CARTESIAN_POINT ( 'NONE',  ( 56.97280603064898941, -277.2763395528616002, -0.4463807625373771293 ) ) ;
#23297=CARTESIAN_POINT ( 'NONE',  ( 109.3153218317886655, 19.84491634189296860, -3.222654707407530239 ) ) ;
#23332=ORIENTED_EDGE ( 'NONE', *, *, #12199, .F. ) ;
#23425=EDGE_CURVE ( 'NONE', #17955, #18253, #33017, .T. ) ;
#23441=CARTESIAN_POINT ( 'NONE',  ( 109.1472041058640912, 18.90877050785832836, -4.999054092451833853 ) ) ;
#23457=ADVANCED_FACE ( 'NONE', ( #12118 ), #20912, .T. ) ;
#23494=CARTESIAN_POINT ( 'NONE',  ( 26.34939556550226314, 19.05368625490716639, -2.334455007174267571 ) ) ;
#23503=CARTESIAN_POINT ( 'NONE',  ( 110.5397548702477764, 21.00556809464028873, 2.806473568333437196 ) ) ;
#23525=EDGE_CURVE ( 'NONE', #2806, #4621, #9143, .T. ) ;
#23526=DIRECTION ( 'NONE',  ( -0.000000000000000000, -0.000000000000000000, -1.000000000000000000 ) ) ;
#23599=CIRCLE ( 'NONE', #27877, 1.800000000000015810 ) ;
#23678=CARTESIAN_POINT ( 'NONE',  ( 109.7266016284592069, 16.47760998941503630, 5.471072653610983494 ) ) ;
#23706=ADVANCED_FACE ( 'NONE', ( #16271 ), #28922, .F. ) ;
#23795=DIRECTION ( 'NONE',  ( -0.000000000000000000, -0.000000000000000000, -1.000000000000000000 ) ) ;
#23801=ORIENTED_EDGE ( 'NONE', *, *, #20488, .F. ) ;
#23812=( NAMED_UNIT ( * ) SI_UNIT ( $, .STERADIAN. ) SOLID_ANGLE_UNIT ( ) );
#23886=ADVANCED_FACE ( 'NONE', ( #709 ), #28409, .T. ) ;
#23909=B_SPLINE_CURVE_WITH_KNOTS ( 'NONE', 3,
 ( #32004, #2079, #14112, #10427 ),
 .UNSPECIFIED., .F., .F.,
 ( 4, 4 ),
 ( 0.000000000000000000, 0.003022500951957912251 ),
 .UNSPECIFIED. ) ;
#24031=DIRECTION ( 'NONE',  ( -0.000000000000000000, -0.000000000000000000, -1.000000000000000000 ) ) ;
#24058=DIRECTION ( 'NONE',  ( 1.000000000000000000, 0.000000000000000000, 0.000000000000000000 ) ) ;
#24083=TOROIDAL_SURFACE ( 'NONE', #18230, 300.0401151713995773, 1.800000000000017142 ) ;
#24084=AXIS2_PLACEMENT_3D ( 'NONE', #11428, #8898, #21624 ) ;
#24154=VECTOR ( 'NONE', #2186, 1000.000000000000227 ) ;
#24177=AXIS2_PLACEMENT_3D ( 'NONE', #1793, #24342, #21826 ) ;
#24188=VECTOR ( 'NONE', #15314, 1000.000000000000000 ) ;
#24191=DIRECTION ( 'NONE',  ( -0.000000000000000000, -0.000000000000000000, -1.000000000000000000 ) ) ;
#24195=DIRECTION ( 'NONE',  ( -0.000000000000000000, -0.000000000000000000, -1.000000000000000000 ) ) ;
#24214=ORIENTED_EDGE ( 'NONE', *, *, #15000, .T. ) ;
#24230=DIRECTION ( 'NONE',  ( 0.9947025833170223263, 0.1027947991993880261, -0.000000000000000000 ) ) ;
#24245=DIRECTION ( 'NONE',  ( 0.000000000000000000, 0.000000000000000000, 1.000000000000000000 ) ) ;
#24269=VERTEX_POINT ( 'NONE', #10982 ) ;
#24342=DIRECTION ( 'NONE',  ( 0.000000000000000000, 0.000000000000000000, 1.000000000000000000 ) ) ;
#24396=ORIENTED_EDGE ( 'NONE', *, *, #29178, .F. ) ;
#24413=DIRECTION ( 'NONE',  ( -0.1027947991993877624, 0.9947025833170222153, 0.000000000000000000 ) ) ;
#24419=ORIENTED_EDGE ( 'NONE', *, *, #8937, .T. ) ;
#24452=ORIENTED_EDGE ( 'NONE', *, *, #19557, .T. ) ;
#24522=CARTESIAN_POINT ( 'NONE',  ( 109.0735342931897378, 18.49854792216788368, 5.381233289707400225 ) ) ;
#24559=AXIS2_PLACEMENT_3D ( 'NONE', #4477, #32550, #9617 ) ;
#24583=EDGE_CURVE ( 'NONE', #28828, #21569, #23208, .T. ) ;
#24604=AXIS2_PLACEMENT_3D ( 'NONE', #18999, #802, #29185 ) ;
#24613=AXIS2_PLACEMENT_3D ( 'NONE', #5597, #20642, #30696 ) ;
#24655=CIRCLE ( 'NONE', #10260, 300.7453860596896220 ) ;
#24663=FACE_OUTER_BOUND ( 'NONE', #22788, .T. ) ;
#24670=DIRECTION ( 'NONE',  ( -1.000000000000000000, 0.000000000000000000, 0.000000000000000000 ) ) ;
#24674=CIRCLE ( 'NONE', #31640, 297.0265809045899346 ) ;
#24683=FACE_OUTER_BOUND ( 'NONE', #12385, .T. ) ;
#24702=ORIENTED_EDGE ( 'NONE', *, *, #1309, .T. ) ;
#24728=VERTEX_POINT ( 'NONE', #11741 ) ;
#24774=ORIENTED_EDGE ( 'NONE', *, *, #18307, .F. ) ;
#24857=CARTESIAN_POINT ( 'NONE',  ( 110.6444052656891301, 21.58830278953161752, 0.4463807625372899768 ) ) ;
#25038=DIRECTION ( 'NONE',  ( -0.1027947991993878596, 0.9947025833170223263, 0.000000000000000000 ) ) ;
#25052=CARTESIAN_POINT ( 'NONE',  ( 109.7606186995332536, 16.66703046365059393, -0.4463807625373608645 ) ) ;
#25056=B_SPLINE_CURVE_WITH_KNOTS ( 'NONE', 3,
 ( #7317, #17507, #11836, #24522, #7169, #22047, #17362, #27702, #6665, #14678 ),
 .UNSPECIFIED., .F., .F.,
 ( 4, 2, 2, 2, 4 ),
 ( 0.000000000000000000, 0.0004294301529276467965, 0.0008588603058552935930, 0.001288290458782940335, 0.001717720611710587186 ),
 .UNSPECIFIED. ) ;
#25068=CARTESIAN_POINT ( 'NONE',  ( 26.44001828968094259, 18.17676778675653892, -2.806473568333506474 ) ) ;
#25114=CIRCLE ( 'NONE', #25651, 5.000000000000001776 ) ;
#25173=AXIS2_PLACEMENT_3D ( 'NONE', #7268, #15281, #9432 ) ;
#25224=TOROIDAL_SURFACE ( 'NONE', #7613, 298.6457063863958865, 5.000000000000000888 ) ;
#25428=DIRECTION ( 'NONE',  ( -0.000000000000000000, -0.000000000000000000, -1.000000000000000000 ) ) ;
#25450=CARTESIAN_POINT ( 'NONE',  ( 56.97280603064898941, -277.2763395528616002, 4.999054092451785891 ) ) ;
#25473=VERTEX_POINT ( 'NONE', #14863 ) ;
#25510=ORIENTED_EDGE ( 'NONE', *, *, #5077, .T. ) ;
#25651=AXIS2_PLACEMENT_3D ( 'NONE', #32771, #30591, #10000 ) ;
#25665=ORIENTED_EDGE ( 'NONE', *, *, #32453, .T. ) ;
#25736=VECTOR ( 'NONE', #3478, 1000.000000000000000 ) ;
#25741=AXIS2_PLACEMENT_3D ( 'NONE', #9020, #29940, #26941 ) ;
#25792=AXIS2_PLACEMENT_3D ( 'NONE', #30671, #15077, #9736 ) ;
#25814=CARTESIAN_POINT ( 'NONE',  ( 109.2312629696829731, 19.37684342964551476, -4.110854402524426021 ) ) ;
#25827=DIRECTION ( 'NONE',  ( -1.000000000000000000, 0.000000000000000000, 0.000000000000000000 ) ) ;
#25835=EDGE_CURVE ( 'NONE', #7000, #19723, #25056, .T. ) ;
#25842=EDGE_CURVE ( 'NONE', #29122, #2806, #19541, .T. ) ;
#25932=EDGE_CURVE ( 'NONE', #15255, #29122, #658, .T. ) ;
#25986=LINE ( 'NONE', #30852, #19193 ) ;
#25988=DIRECTION ( 'NONE',  ( -0.000000000000000000, -0.000000000000000000, -1.000000000000000000 ) ) ;
#26028=ORIENTED_EDGE ( 'NONE', *, *, #22495, .T. ) ;
#26207=SHAPE_DEFINITION_REPRESENTATION ( #7355, #6656 ) ;
#26280=CIRCLE ( 'NONE', #16113, 301.6269746700523342 ) ;
#26285=DIRECTION ( 'NONE',  ( -0.9947025833170222153, -0.1027947991993880122, 0.000000000000000000 ) ) ;
#26326=AXIS2_PLACEMENT_3D ( 'NONE', #5121, #17138, #1960 ) ;
#26614=ORIENTED_EDGE ( 'NONE', *, *, #15967, .F. ) ;
#26633=DIRECTION ( 'NONE',  ( -0.04852105321274841065, 0.4695180821586825148, 0.8815886103626556780 ) ) ;
#26664=LINE ( 'NONE', #23503, #25736 ) ;
#26718=ORIENTED_EDGE ( 'NONE', *, *, #27807, .F. ) ;
#26721=AXIS2_PLACEMENT_3D ( 'NONE', #1964, #17331, #6633 ) ;
#26803=EDGE_LOOP ( 'NONE', ( #688, #305, #27635, #12100 ) ) ;
#26823=LINE ( 'NONE', #11606, #19238 ) ;
#26848=CIRCLE ( 'NONE', #4435, 5.000000000000001776 ) ;
#26873=LINE ( 'NONE', #1470, #17707 ) ;
#26941=DIRECTION ( 'NONE',  ( -0.1027947991993877902, 0.9947025833170222153, 0.000000000000000000 ) ) ;
#27014=VERTEX_POINT ( 'NONE', #29769 ) ;
#27054=LINE ( 'NONE', #32272, #30631 ) ;
#27101=EDGE_LOOP ( 'NONE', ( #23332, #7628, #13432, #17993 ) ) ;
#27268=FACE_OUTER_BOUND ( 'NONE', #12317, .T. ) ;
#27334=CIRCLE ( 'NONE', #641, 302.6457063863958865 ) ;
#27363=DIRECTION ( 'NONE',  ( -0.000000000000000000, -0.000000000000000000, -1.000000000000000000 ) ) ;
#27375=CIRCLE ( 'NONE', #5508, 5.000000000000000000 ) ;
#27424=ORIENTED_EDGE ( 'NONE', *, *, #27663, .T. ) ;
#27445=DIRECTION ( 'NONE',  ( -0.1767573132311699990, -0.9842544651762054064, 0.000000000000000000 ) ) ;
#27494=ORIENTED_EDGE ( 'NONE', *, *, #32263, .F. ) ;
#27534=ORIENTED_EDGE ( 'NONE', *, *, #27856, .F. ) ;
#27635=ORIENTED_EDGE ( 'NONE', *, *, #23525, .F. ) ;
#27654=DIRECTION ( 'NONE',  ( -1.000000000000000000, 0.000000000000000000, 0.000000000000000000 ) ) ;
#27663=EDGE_CURVE ( 'NONE', #2795, #3368, #29816, .T. ) ;
#27702=CARTESIAN_POINT ( 'NONE',  ( 108.9281931508044181, 17.68923109249016790, 5.234450355725419612 ) ) ;
#27788=ADVANCED_FACE ( 'NONE', ( #20199 ), #14986, .F. ) ;
#27795=ORIENTED_EDGE ( 'NONE', *, *, #25835, .T. ) ;
#27807=EDGE_CURVE ( 'NONE', #16263, #8590, #15681, .T. ) ;
#27856=EDGE_CURVE ( 'NONE', #27014, #18253, #29033, .T. ) ;
#27877=AXIS2_PLACEMENT_3D ( 'NONE', #30314, #7389, #15400 ) ;
#27882=CARTESIAN_POINT ( 'NONE',  ( 110.2535626002996310, 19.41193660949216238, 0.4463807625373348298 ) ) ;
#27886=ORIENTED_EDGE ( 'NONE', *, *, #7087, .T. ) ;
#27963=AXIS2_PLACEMENT_3D ( 'NONE', #10418, #20777, #30980 ) ;
#28092=DIRECTION ( 'NONE',  ( -0.1767573132311711093, -0.9842544651762052954, 0.000000000000000000 ) ) ;
#28207=DIRECTION ( 'NONE',  ( 0.08343273266574956215, 0.4645863764670183360, 0.8815886103626631165 ) ) ;
#28329=VERTEX_POINT ( 'NONE', #13428 ) ;
#28339=ORIENTED_EDGE ( 'NONE', *, *, #5326, .T. ) ;
#28381=CIRCLE ( 'NONE', #8609, 5.000000000000001776 ) ;
#28382=ORIENTED_EDGE ( 'NONE', *, *, #6090, .T. ) ;
#28409=CONICAL_SURFACE ( 'NONE', #17730, 299.3348442831094189, 0.4915790642873356098 ) ;
#28418=CIRCLE ( 'NONE', #14415, 1.799999999999977174 ) ;
#28490=VECTOR ( 'NONE', #26633, 1000.000000000000114 ) ;
#28540=LINE ( 'NONE', #31522, #30678 ) ;
#28550=CARTESIAN_POINT ( 'NONE',  ( 56.97280603064898941, -277.2763395528616002, 0.4463807625373211185 ) ) ;
#28672=SHAPE_REPRESENTATION_RELATIONSHIP ( 'NONE' , 'NONE' ,  #6656, #2414 ) ;
#28695=DIRECTION ( 'NONE',  ( -0.08343273266574513514, -0.4645863764670032925, -0.8815886103626715542 ) ) ;
#28717=CARTESIAN_POINT ( 'NONE',  ( 56.97280603064898941, -277.2763395528616002, 0.4463807625373084065 ) ) ;
#28721=CARTESIAN_POINT ( 'NONE',  ( 56.97280603064898941, -277.2763395528616002, 0.000000000000000000 ) ) ;
#28807=VECTOR ( 'NONE', #14927, 1000.000000000000000 ) ;
#28814=VERTEX_POINT ( 'NONE', #30428 ) ;
#28828=VERTEX_POINT ( 'NONE', #32793 ) ;
#28888=DIRECTION ( 'NONE',  ( -1.000000000000000000, 0.000000000000000000, 0.000000000000000000 ) ) ;
#28922=TOROIDAL_SURFACE ( 'NONE', #24084, 301.4345239564033250, 3.999999999999999112 ) ;
#28968=ORIENTED_EDGE ( 'NONE', *, *, #10267, .F. ) ;
#28970=AXIS2_PLACEMENT_3D ( 'NONE', #6995, #9167, #12178 ) ;
#29033=CIRCLE ( 'NONE', #30099, 296.4345239564032113 ) ;
#29063=DIRECTION ( 'NONE',  ( -1.000000000000000000, 0.000000000000000000, 0.000000000000000000 ) ) ;
#29068=CARTESIAN_POINT ( 'NONE',  ( 110.5397548702477764, 21.00556809464030650, 2.806473568333438084 ) ) ;
#29122=VERTEX_POINT ( 'NONE', #3116 ) ;
#29131=CARTESIAN_POINT ( 'NONE',  ( 56.97280603064898941, -277.2763395528616002, 0.000000000000000000 ) ) ;
#29139=ORIENTED_EDGE ( 'NONE', *, *, #7336, .F. ) ;
#29178=EDGE_CURVE ( 'NONE', #4283, #28828, #29883, .T. ) ;
#29185=DIRECTION ( 'NONE',  ( 0.1767573132311711093, 0.9842544651762052954, 0.000000000000000000 ) ) ;
#29210=CYLINDRICAL_SURFACE ( 'NONE', #16749, 296.4345239564032681 ) ;
#29245=EDGE_LOOP ( 'NONE', ( #31687, #20502, #12749, #23105, #10195, #15422, #11686, #23801, #9074, #20806, #14854, #31567 ) ) ;
#29291=DIRECTION ( 'NONE',  ( 0.9947025833170223263, 0.1027947991993880261, 0.000000000000000000 ) ) ;
#29371=CARTESIAN_POINT ( 'NONE',  ( 25.82046699000660439, 24.17190842697641529, 2.806473568333438084 ) ) ;
#29378=AXIS2_PLACEMENT_3D ( 'NONE', #17493, #15164, #14972 ) ;
#29401=CARTESIAN_POINT ( 'NONE',  ( 26.27358061090003361, 19.78731608622335969, -0.4463807625373608645 ) ) ;
#29402=EDGE_CURVE ( 'NONE', #29122, #19723, #20926, .T. ) ;
#29408=ORIENTED_EDGE ( 'NONE', *, *, #29178, .T. ) ;
#29418=CIRCLE ( 'NONE', #24604, 5.000000000000001776 ) ;
#29490=CARTESIAN_POINT ( 'NONE',  ( 108.8978791464556508, 17.52043075494136204, -4.999054092451819642 ) ) ;
#29526=VECTOR ( 'NONE', #5139, 1000.000000000000000 ) ;
#29678=DIRECTION ( 'NONE',  ( 1.000000000000000000, -3.540392581751473016E-15, 0.000000000000000000 ) ) ;
#29722=CARTESIAN_POINT ( 'NONE',  ( 109.4744264295851082, 15.07339897850246224, -2.806473568333505586 ) ) ;
#29740=CARTESIAN_POINT ( 'NONE',  ( 109.4831014662948974, 20.77917954950586577, -0.4463807625373443777 ) ) ;
#29753=FACE_OUTER_BOUND ( 'NONE', #12315, .T. ) ;
#29769=CARTESIAN_POINT ( 'NONE',  ( 26.50087866478441256, 17.58784721092444769, -0.4463807625373593657 ) ) ;
#29816=LINE ( 'NONE', #6241, #28490 ) ;
#29876=DIRECTION ( 'NONE',  ( -1.000000000000000000, 0.000000000000000000, 0.000000000000000000 ) ) ;
#29883=CIRCLE ( 'NONE', #3213, 302.6457063863960002 ) ;
#29938=VERTEX_POINT ( 'NONE', #20019 ) ;
#29940=DIRECTION ( 'NONE',  ( -0.000000000000000000, -0.000000000000000000, -1.000000000000000000 ) ) ;
#29941=ORIENTED_EDGE ( 'NONE', *, *, #4425, .T. ) ;
#29943=DIRECTION ( 'NONE',  ( -0.000000000000000000, -0.000000000000000000, -1.000000000000000000 ) ) ;
#29956=TOROIDAL_SURFACE ( 'NONE', #15530, 300.0401151713995773, 0.8000000000000170308 ) ;
#30022=AXIS2_PLACEMENT_3D ( 'NONE', #160, #24191, #29063 ) ;
#30027=CARTESIAN_POINT ( 'NONE',  ( 56.97280603064898941, -277.2763395528616002, 0.4463807625373157340 ) ) ;
#30037=FACE_OUTER_BOUND ( 'NONE', #26803, .T. ) ;
#30053=FACE_OUTER_BOUND ( 'NONE', #10852, .T. ) ;
#30099=AXIS2_PLACEMENT_3D ( 'NONE', #2329, #10490, #23214 ) ;
#30114=ORIENTED_EDGE ( 'NONE', *, *, #17940, .F. ) ;
#30137=DIRECTION ( 'NONE',  ( -0.1027947991993878180, 0.9947025833170221043, 0.000000000000000000 ) ) ;
#30149=DIRECTION ( 'NONE',  ( -1.000000000000000000, 0.000000000000000000, 0.000000000000000000 ) ) ;
#30239=UNCERTAINTY_MEASURE_WITH_UNIT (LENGTH_MEASURE( 1.000000000000000082E-05 ), #7794, 'distance_accuracy_value', 'NONE');
#30314=CARTESIAN_POINT ( 'NONE',  ( 26.13024263984378592, 21.17433810686643980, 4.621439243524390506 ) ) ;
#30396=DIRECTION ( 'NONE',  ( -0.9842544651762054064, 0.1767573132311699990, 0.000000000000000000 ) ) ;
#30408=CARTESIAN_POINT ( 'NONE',  ( 109.1350892577483620, 18.84131025325909548, -5.127064439618892244 ) ) ;
#30428=CARTESIAN_POINT ( 'NONE',  ( 26.50087866478441256, 17.58784721092444769, 0.4463807625373157340 ) ) ;
#30522=CARTESIAN_POINT ( 'NONE',  ( 109.4831014662949258, 20.77917954950597235, 0.7764623220122568448 ) ) ;
#30569=ORIENTED_EDGE ( 'NONE', *, *, #5077, .F. ) ;
#30581=CARTESIAN_POINT ( 'NONE',  ( 56.97280603064898941, -277.2763395528616002, 5.471072653610979941 ) ) ;
#30591=DIRECTION ( 'NONE',  ( 0.9842544651762055175, -0.1767573132311700268, 0.000000000000000000 ) ) ;
#30610=( GEOMETRIC_REPRESENTATION_CONTEXT ( 3 ) GLOBAL_UNCERTAINTY_ASSIGNED_CONTEXT ( ( #30239 ) ) GLOBAL_UNIT_ASSIGNED_CONTEXT ( ( #7794, #17986, #23812 ) ) REPRESENTATION_CONTEXT ( 'NONE', 'WORKASPACE' ) );
#30629=VERTEX_POINT ( 'NONE', #1039 ) ;
#30631=VECTOR ( 'NONE', #8840, 1000.000000000000227 ) ;
#30671=CARTESIAN_POINT ( 'NONE',  ( 56.97280603064898941, -277.2763395528616002, -0.4463807625373593657 ) ) ;
#30678=VECTOR ( 'NONE', #5465, 1000.000000000000000 ) ;
#30696=DIRECTION ( 'NONE',  ( -0.1027947991993879290, 0.9947025833170223263, 0.000000000000000000 ) ) ;
#30705=DIRECTION ( 'NONE',  ( 0.1027947991993878873, -0.9947025833170223263, 4.441163149043747538E-14 ) ) ;
#30768=DIRECTION ( 'NONE',  ( -0.000000000000000000, -0.000000000000000000, -1.000000000000000000 ) ) ;
#30830=DIRECTION ( 'NONE',  ( -0.000000000000000000, -0.000000000000000000, -1.000000000000000000 ) ) ;
#30852=CARTESIAN_POINT ( 'NONE',  ( 56.97280603064904625, -277.2763395528616002, 566.7009208965938569 ) ) ;
#30909=VERTEX_POINT ( 'NONE', #6330 ) ;
#30930=CARTESIAN_POINT ( 'NONE',  ( 108.5619817448483531, 15.65002148400668247, -0.4463807625373593657 ) ) ;
#30934=CARTESIAN_POINT ( 'NONE',  ( 109.3697760341437970, 14.49066428361112813, -0.4463807625373593657 ) ) ;
#30972=EDGE_LOOP ( 'NONE', ( #5599, #20854, #27534, #5781 ) ) ;
#30975=FACE_OUTER_BOUND ( 'NONE', #10111, .T. ) ;
#30980=DIRECTION ( 'NONE',  ( -1.000000000000000000, 0.000000000000000000, 0.000000000000000000 ) ) ;
#31006=DIRECTION ( 'NONE',  ( 0.9947025833170223263, 0.1027947991993880261, -0.000000000000000000 ) ) ;
#31018=TOROIDAL_SURFACE ( 'NONE', #2177, 300.0401151713995773, 1.799999999999978728 ) ;
#31068=AXIS2_PLACEMENT_3D ( 'NONE', #16837, #17158, #9126 ) ;
#31084=EDGE_CURVE ( 'NONE', #19335, #8885, #12111, .T. ) ;
#31094=ORIENTED_EDGE ( 'NONE', *, *, #18789, .F. ) ;
#31098=CARTESIAN_POINT ( 'NONE',  ( 108.5970690979676334, 15.84540171098336714, -1.732900873336792547 ) ) ;
#31108=CARTESIAN_POINT ( 'NONE',  ( 56.97280603064898941, -277.2763395528616002, -0.4463807625373608645 ) ) ;
#31158=ORIENTED_EDGE ( 'NONE', *, *, #19557, .F. ) ;
#31234=DIRECTION ( 'NONE',  ( -1.000000000000000000, 0.000000000000000000, 0.000000000000000000 ) ) ;
#31265=VERTEX_POINT ( 'NONE', #3608 ) ;
#31267=DIRECTION ( 'NONE',  ( -0.000000000000000000, -0.000000000000000000, -1.000000000000000000 ) ) ;
#31328=EDGE_CURVE ( 'NONE', #2806, #15877, #4446, .T. ) ;
#31409=ORIENTED_EDGE ( 'NONE', *, *, #17119, .T. ) ;
#31522=CARTESIAN_POINT ( 'NONE',  ( 26.29336354336543735, 19.59588486419533382, 5.471072653610983494 ) ) ;
#31550=CIRCLE ( 'NONE', #17120, 5.000000000000001776 ) ;
#31553=EDGE_CURVE ( 'NONE', #469, #16936, #17247, .T. ) ;
#31564=DIRECTION ( 'NONE',  ( -0.04852105321274532979, 0.4695180821586686926, 0.8815886103626632275 ) ) ;
#31567=ORIENTED_EDGE ( 'NONE', *, *, #11244, .F. ) ;
#31640=AXIS2_PLACEMENT_3D ( 'NONE', #32807, #5352, #4855 ) ;
#31687=ORIENTED_EDGE ( 'NONE', *, *, #22874, .F. ) ;
#31711=PRODUCT_DEFINITION ( 'UNKNOWN', '', #7706, #16583 ) ;
#31731=ORIENTED_EDGE ( 'NONE', *, *, #20802, .T. ) ;
#31741=DIRECTION ( 'NONE',  ( 0.1767573132311666129, 0.9842544651762059615, 0.000000000000000000 ) ) ;
#31755=FACE_OUTER_BOUND ( 'NONE', #14224, .T. ) ;
#31791=ORIENTED_EDGE ( 'NONE', *, *, #9823, .F. ) ;
#31858=ORIENTED_EDGE ( 'NONE', *, *, #15298, .F. ) ;
#31861=EDGE_CURVE ( 'NONE', #28329, #28828, #15884, .T. ) ;
#31908=CARTESIAN_POINT ( 'NONE',  ( 56.97280603064898941, -277.2763395528616002, -4.999054092451833853 ) ) ;
#31956=FACE_OUTER_BOUND ( 'NONE', #32043, .T. ) ;
#32004=CARTESIAN_POINT ( 'NONE',  ( 108.6457025336241031, 16.11621187055573046, -2.334455007174250696 ) ) ;
#32035=DIRECTION ( 'NONE',  ( -0.000000000000000000, -0.000000000000000000, -1.000000000000000000 ) ) ;
#32043=EDGE_LOOP ( 'NONE', ( #30569, #18281, #12417, #23004 ) ) ;
#32066=CIRCLE ( 'NONE', #3249, 298.4532556727466499 ) ;
#32163=AXIS2_PLACEMENT_3D ( 'NONE', #9553, #32836, #12580 ) ;
#32215=DIRECTION ( 'NONE',  ( -0.1027947991993878041, 0.9947025833170222153, 0.000000000000000000 ) ) ;
#32263=EDGE_CURVE ( 'NONE', #18451, #8590, #2799, .T. ) ;
#32272=CARTESIAN_POINT ( 'NONE',  ( 25.82046699000660439, 24.17190842697641173, 2.806473568333437196 ) ) ;
#32301=ADVANCED_FACE ( 'NONE', ( #31956 ), #9714, .F. ) ;
#32368=CARTESIAN_POINT ( 'NONE',  ( 26.50087866478441256, 17.58784721092446190, 0.4463807625373157340 ) ) ;
#32408=CARTESIAN_POINT ( 'NONE',  ( 25.91108971418529805, 23.29498995882582335, -2.334455007174283558 ) ) ;
#32410=CARTESIAN_POINT ( 'NONE',  ( 108.5692966685781755, 15.69075386566562713, 1.106576256426021532 ) ) ;
#32416=EDGE_LOOP ( 'NONE', ( #13200, #17633, #7291, #6494 ) ) ;
#32426=EDGE_CURVE ( 'NONE', #24269, #25473, #24674, .T. ) ;
#32453=EDGE_CURVE ( 'NONE', #4554, #469, #17402, .T. ) ;
#32477=DIRECTION ( 'NONE',  ( -0.000000000000000000, -0.000000000000000000, -1.000000000000000000 ) ) ;
#32550=DIRECTION ( 'NONE',  ( 0.000000000000000000, 0.000000000000000000, 1.000000000000000000 ) ) ;
#32639=ORIENTED_EDGE ( 'NONE', *, *, #24583, .T. ) ;
#32691=AXIS2_PLACEMENT_3D ( 'NONE', #28550, #15969, #31234 ) ;
#32722=FACE_OUTER_BOUND ( 'NONE', #22207, .T. ) ;
#32771=CARTESIAN_POINT ( 'NONE',  ( 109.7606186995332536, 16.66703046365059393, 0.4463807625373084065 ) ) ;
#32793=CARTESIAN_POINT ( 'NONE',  ( 109.4831014662949258, 20.77917954950597590, 0.4463807625372899768 ) ) ;
#32807=CARTESIAN_POINT ( 'NONE',  ( 56.97280603064898941, -277.2763395528616002, 2.806473568333413660 ) ) ;
#32836=DIRECTION ( 'NONE',  ( 0.9947025833170223263, 0.1027947991993880261, -0.000000000000000000 ) ) ;
#32964=ADVANCED_FACE ( 'NONE', ( #24663 ), #12971, .T. ) ;
#32990=DIRECTION ( 'NONE',  ( -1.000000000000000000, 0.000000000000000000, 0.000000000000000000 ) ) ;
#33005=ORIENTED_EDGE ( 'NONE', *, *, #8207, .T. ) ;
#33017=LINE ( 'NONE', #4604, #19837 ) ;
#33040=ORIENTED_EDGE ( 'NONE', *, *, #14685, .T. ) ;
#33048=LINE ( 'NONE', #2122, #24188 ) ;
#33066=ADVANCED_FACE ( 'NONE', ( #30037 ), #17765, .F. ) ;
#33079=CARTESIAN_POINT ( 'NONE',  ( 108.9970757964848076, 18.07279684343247439, -5.421406142183877286 ) ) ;
#33106=COLOUR_RGB('Deep Blue', 0.66274510, 0.83137255, 0.94901961);
#33107=FILL_AREA_STYLE_COLOUR('',#33106);
#33108=FILL_AREA_STYLE('',(#33107));
#33109=SURFACE_STYLE_FILL_AREA(#33108);
#33110=SURFACE_SIDE_STYLE('',(#33109));
#33111=SURFACE_STYLE_USAGE(.BOTH.,#33110);
#33112=PRESENTATION_STYLE_ASSIGNMENT((#33111));
#33148=STYLED_ITEM('',(#33112),#9961);
#33149=MECHANICAL_DESIGN_GEOMETRIC_PRESENTATION_REPRESENTATION('',(#33148),#30610);
ENDSEC;
END-ISO-10303-21;
